ISO-10303-21;
HEADER;
FILE_DESCRIPTION (('STEP AP203'),
    '1' );
FILE_NAME ('Spool_Varsayılan.step',
    '2026-10-08T23:54:15',
    ( '' ),
    ( '' ),
    'SwSTEP 2.0',
    'SolidWorks 2024',
    '' );
FILE_SCHEMA (( 'AUTOMOTIVE_DESIGN' ));
ENDSEC;

DATA;
#27=LINE ( 'NONE', #61937, #7762 ) ;
#83=ADVANCED_FACE ( 'NONE', ( #38389 ), #14547, .F. ) ;
#323=VECTOR ( 'NONE', #80047, 1000.000000000000000 ) ;
#580=SHAPE_DEFINITION_REPRESENTATION ( #87904, #55609 ) ;
#647=VERTEX_POINT ( 'NONE', #21533 ) ;
#649=EDGE_CURVE ( 'NONE', #44273, #78408, #52510, .T. ) ;
#663=CARTESIAN_POINT ( 'NONE',  ( 0.6000000000000007550, 0.000000000000000000, 24.00000000000000000 ) ) ;
#672=LINE ( 'NONE', #31619, #25422 ) ;
#771=CARTESIAN_POINT ( 'NONE',  ( -5.366453405989236813, -2.000000000000001776, 19.19609335255483984 ) ) ;
#840=DIRECTION ( 'NONE',  ( -1.000000000000000000, -0.000000000000000000, -0.000000000000000000 ) ) ;
#912=AXIS2_PLACEMENT_3D ( 'NONE', #19260, #5043, #27389 ) ;
#928=ORIENTED_EDGE ( 'NONE', *, *, #10258, .T. ) ;
#1133=CARTESIAN_POINT ( 'NONE',  ( 16.00000000000000000, 2.681976490132703452E-15, -21.89999999999999858 ) ) ;
#1521=EDGE_LOOP ( 'NONE', ( #83273, #73807, #76093, #78613 ) ) ;
#1533=CARTESIAN_POINT ( 'NONE',  ( 0.000000000000000000, 0.000000000000000000, 0.000000000000000000 ) ) ;
#1592=DIRECTION ( 'NONE',  ( -0.000000000000000000, 0.000000000000000000, 1.000000000000000000 ) ) ;
#1755=DIRECTION ( 'NONE',  ( 0.000000000000000000, 0.000000000000000000, 1.000000000000000000 ) ) ;
#1763=VERTEX_POINT ( 'NONE', #13444 ) ;
#2037=CARTESIAN_POINT ( 'NONE',  ( 7.150000000000004796, -2.000000000000001776, 24.00000000000000000 ) ) ;
#2293=ORIENTED_EDGE ( 'NONE', *, *, #35247, .T. ) ;
#2428=ORIENTED_EDGE ( 'NONE', *, *, #23303, .T. ) ;
#2504=ADVANCED_FACE ( 'NONE', ( #96453 ), #57912, .T. ) ;
#2594=EDGE_CURVE ( 'NONE', #78412, #30953, #82222, .T. ) ;
#2722=CARTESIAN_POINT ( 'NONE',  ( -5.366453405989236813, 0.000000000000000000, 0.000000000000000000 ) ) ;
#2825=ORIENTED_EDGE ( 'NONE', *, *, #90659, .F. ) ;
#2843=DIRECTION ( 'NONE',  ( -1.000000000000000000, -0.000000000000000000, -0.000000000000000000 ) ) ;
#2877=EDGE_CURVE ( 'NONE', #85731, #78408, #82252, .T. ) ;
#2943=VERTEX_POINT ( 'NONE', #27325 ) ;
#3041=DIRECTION ( 'NONE',  ( 0.000000000000000000, 0.000000000000000000, -1.000000000000000000 ) ) ;
#3071=PLANE ( 'NONE',  #18985 ) ;
#3108=ORIENTED_EDGE ( 'NONE', *, *, #23303, .F. ) ;
#3226=VECTOR ( 'NONE', #72604, 1000.000000000000000 ) ;
#3292=EDGE_CURVE ( 'NONE', #46565, #42982, #90597, .T. ) ;
#3319=ORIENTED_EDGE ( 'NONE', *, *, #51851, .T. ) ;
#3371=DIRECTION ( 'NONE',  ( 0.000000000000000000, 0.000000000000000000, 1.000000000000000000 ) ) ;
#3421=ORIENTED_EDGE ( 'NONE', *, *, #59697, .F. ) ;
#3594=CARTESIAN_POINT ( 'NONE',  ( 7.150000000000004796, -2.000000000000001776, 24.00000000000000000 ) ) ;
#3801=CIRCLE ( 'NONE', #76690, 18.35000000000000142 ) ;
#3876=ORIENTED_EDGE ( 'NONE', *, *, #37712, .F. ) ;
#3968=CARTESIAN_POINT ( 'NONE',  ( -5.366453405989235925, -2.000000000000005329, 18.24068255301867936 ) ) ;
#3995=VECTOR ( 'NONE', #34910, 1000.000000000000000 ) ;
#4000=DIRECTION ( 'NONE',  ( -1.000000000000000000, -0.000000000000000000, -0.000000000000000000 ) ) ;
#4044=EDGE_LOOP ( 'NONE', ( #94980, #47371 ) ) ;
#4061=DIRECTION ( 'NONE',  ( 2.710505431213760099E-16, -1.000000000000000000, 0.000000000000000000 ) ) ;
#4178=DIRECTION ( 'NONE',  ( -1.000000000000000000, -0.000000000000000000, -0.000000000000000000 ) ) ;
#4205=CARTESIAN_POINT ( 'NONE',  ( -5.366453405989236813, 0.000000000000000000, 0.000000000000000000 ) ) ;
#4263=ORIENTED_EDGE ( 'NONE', *, *, #37712, .T. ) ;
#4380=EDGE_LOOP ( 'NONE', ( #22061, #91754, #10612, #10485 ) ) ;
#4381=CARTESIAN_POINT ( 'NONE',  ( 0.000000000000000000, 0.000000000000000000, 4.450000000000000178 ) ) ;
#4384=LINE ( 'NONE', #58661, #21940 ) ;
#4399=EDGE_LOOP ( 'NONE', ( #22097, #14597, #15336, #18356 ) ) ;
#4471=ADVANCED_FACE ( 'NONE', ( #73638 ), #75124, .F. ) ;
#4719=ADVANCED_FACE ( 'NONE', ( #78610, #40075 ), #64443, .F. ) ;
#4777=ORIENTED_EDGE ( 'NONE', *, *, #20848, .T. ) ;
#4974=EDGE_LOOP ( 'NONE', ( #70293, #99122, #52309, #56768 ) ) ;
#5043=DIRECTION ( 'NONE',  ( -1.000000000000000000, -0.000000000000000000, -0.000000000000000000 ) ) ;
#5086=DIRECTION ( 'NONE',  ( 1.000000000000000000, 0.000000000000000000, 0.000000000000000000 ) ) ;
#5097=EDGE_CURVE ( 'NONE', #44273, #17897, #49665, .T. ) ;
#5186=DIRECTION ( 'NONE',  ( 0.000000000000000000, 0.000000000000000000, -1.000000000000000000 ) ) ;
#5212=ORIENTED_EDGE ( 'NONE', *, *, #52682, .T. ) ;
#5242=AXIS2_PLACEMENT_3D ( 'NONE', #38361, #46480, #16016 ) ;
#5270=ORIENTED_EDGE ( 'NONE', *, *, #11720, .F. ) ;
#5399=ORIENTED_EDGE ( 'NONE', *, *, #89415, .T. ) ;
#5542=AXIS2_PLACEMENT_3D ( 'NONE', #88739, #98321, #96342 ) ;
#5590=DIRECTION ( 'NONE',  ( 0.000000000000000000, 2.664535259100375697E-15, 1.000000000000000000 ) ) ;
#5603=AXIS2_PLACEMENT_3D ( 'NONE', #76460, #6967, #37918 ) ;
#5749=DIRECTION ( 'NONE',  ( -1.000000000000000000, -0.000000000000000000, -0.000000000000000000 ) ) ;
#5761=ORIENTED_EDGE ( 'NONE', *, *, #2594, .F. ) ;
#5772=DIRECTION ( 'NONE',  ( -1.654368437580061084E-16, 1.000000000000000000, 2.664535259100375697E-15 ) ) ;
#5867=ORIENTED_EDGE ( 'NONE', *, *, #20848, .F. ) ;
#6192=EDGE_CURVE ( 'NONE', #66070, #2943, #25446, .T. ) ;
#6251=ORIENTED_EDGE ( 'NONE', *, *, #649, .T. ) ;
#6281=CARTESIAN_POINT ( 'NONE',  ( -5.366453405989236813, 2.681976490132703452E-15, -21.89999999999999858 ) ) ;
#6339=FACE_OUTER_BOUND ( 'NONE', #4380, .T. ) ;
#6406=( BOUNDED_CURVE ( )  B_SPLINE_CURVE ( 3, ( #75774, #60085, #44851, #37231 ),
 .UNSPECIFIED., .F., .T. ) 
 B_SPLINE_CURVE_WITH_KNOTS ( ( 4, 4 ),
 ( 1.466983014708610034, 1.570796326794896558 ),
 .UNSPECIFIED. ) 
 CURVE ( )  GEOMETRIC_REPRESENTATION_ITEM ( )  RATIONAL_B_SPLINE_CURVE ( ( 1.000000000000000000, 0.9991021013140741758, 0.9991021013140741758, 1.000000000000000000 ) ) 
 REPRESENTATION_ITEM ( '' )  );
#6410=CARTESIAN_POINT ( 'NONE',  ( 1.999999999999998224, 0.000000000000000000, 0.000000000000000000 ) ) ;
#6640=DIRECTION ( 'NONE',  ( -0.2425356250363331356, -0.9701425001453318764, 0.000000000000000000 ) ) ;
#6717=PLANE ( 'NONE',  #25815 ) ;
#6808=CARTESIAN_POINT ( 'NONE',  ( 10.28385788129874001, 1.335431525194933577, 19.26533332368850182 ) ) ;
#6817=CARTESIAN_POINT ( 'NONE',  ( -5.366453405989236813, 0.000000000000000000, 18.35000000000000142 ) ) ;
#6920=ORIENTED_EDGE ( 'NONE', *, *, #78393, .F. ) ;
#6967=DIRECTION ( 'NONE',  ( -0.000000000000000000, 1.000000000000000000, 0.000000000000000000 ) ) ;
#7045=EDGE_CURVE ( 'NONE', #20245, #58804, #35026, .T. ) ;
#7209=ORIENTED_EDGE ( 'NONE', *, *, #78573, .F. ) ;
#7249=LINE ( 'NONE', #61566, #97286 ) ;
#7287=ORIENTED_EDGE ( 'NONE', *, *, #81984, .T. ) ;
#7319=EDGE_CURVE ( 'NONE', #94825, #43365, #81152, .T. ) ;
#7390=DIRECTION ( 'NONE',  ( 0.000000000000000000, 0.000000000000000000, 1.000000000000000000 ) ) ;
#7482=EDGE_LOOP ( 'NONE', ( #54312, #64331, #3876, #29456 ) ) ;
#7565=AXIS2_PLACEMENT_3D ( 'NONE', #14631, #30358, #17006 ) ;
#7591=CARTESIAN_POINT ( 'NONE',  ( 1.600000000000000755, 0.000000000000000000, 0.000000000000000000 ) ) ;
#7762=VECTOR ( 'NONE', #70541, 1000.000000000000000 ) ;
#7771=VECTOR ( 'NONE', #41760, 1000.000000000000000 ) ;
#7889=CARTESIAN_POINT ( 'NONE',  ( 15.00000000000000533, 0.000000000000000000, 0.000000000000000000 ) ) ;
#7929=PLANE ( 'NONE',  #37896 ) ;
#7941=VERTEX_POINT ( 'NONE', #24122 ) ;
#7945=EDGE_CURVE ( 'NONE', #48682, #89740, #14511, .T. ) ;
#7993=CARTESIAN_POINT ( 'NONE',  ( -5.366453405989236813, 0.000000000000000000, 0.000000000000000000 ) ) ;
#8023=CARTESIAN_POINT ( 'NONE',  ( 0.3000000000000007661, 0.000000000000000000, 18.50000000000000000 ) ) ;
#8077=ORIENTED_EDGE ( 'NONE', *, *, #52665, .T. ) ;
#8189=DIRECTION ( 'NONE',  ( -1.000000000000000000, -0.000000000000000000, -0.000000000000000000 ) ) ;
#8492=CARTESIAN_POINT ( 'NONE',  ( 6.150000000000003908, 1.999999999999998224, 18.24068255301868291 ) ) ;
#8635=DIRECTION ( 'NONE',  ( 0.000000000000000000, 0.000000000000000000, -1.000000000000000000 ) ) ;
#8708=CARTESIAN_POINT ( 'NONE',  ( 16.30000000000000071, 0.000000000000000000, 18.35000000000000142 ) ) ;
#8891=ORIENTED_EDGE ( 'NONE', *, *, #62740, .T. ) ;
#8933=EDGE_CURVE ( 'NONE', #15581, #29598, #18639, .T. ) ;
#8968=LINE ( 'NONE', #78972, #96580 ) ;
#8994=CYLINDRICAL_SURFACE ( 'NONE', #74677, 24.00000000000000000 ) ;
#9044=EDGE_LOOP ( 'NONE', ( #3421, #68783 ) ) ;
#9083=DIRECTION ( 'NONE',  ( 0.000000000000000000, 0.000000000000000000, 1.000000000000000000 ) ) ;
#9127=EDGE_LOOP ( 'NONE', ( #2825, #46985 ) ) ;
#9186=FACE_BOUND ( 'NONE', #4044, .T. ) ;
#9231=ORIENTED_EDGE ( 'NONE', *, *, #22296, .F. ) ;
#9286=ADVANCED_FACE ( 'NONE', ( #68322 ), #60723, .T. ) ;
#9291=CIRCLE ( 'NONE', #91934, 18.35000000000000142 ) ;
#9378=LINE ( 'NONE', #771, #85702 ) ;
#9397=ORIENTED_EDGE ( 'NONE', *, *, #84248, .T. ) ;
#9524=EDGE_LOOP ( 'NONE', ( #9397, #15137 ) ) ;
#9594=CARTESIAN_POINT ( 'NONE',  ( 0.000000000000000000, 6.099999999999999645, 0.000000000000000000 ) ) ;
#9607=DIRECTION ( 'NONE',  ( 0.000000000000000000, 0.000000000000000000, -1.000000000000000000 ) ) ;
#9698=EDGE_CURVE ( 'NONE', #20703, #67226, #42571, .T. ) ;
#9966=CARTESIAN_POINT ( 'NONE',  ( 6.150000000000003908, 1.999999999999998224, 24.00000000000000000 ) ) ;
#10224=AXIS2_PLACEMENT_3D ( 'NONE', #91806, #60388, #91311 ) ;
#10242=ORIENTED_EDGE ( 'NONE', *, *, #35008, .F. ) ;
#10258=EDGE_CURVE ( 'NONE', #89740, #89130, #79843, .T. ) ;
#10405=EDGE_LOOP ( 'NONE', ( #37519, #78111, #33704, #20880 ) ) ;
#10477=CARTESIAN_POINT ( 'NONE',  ( -5.366453405989236813, 0.000000000000000000, 0.000000000000000000 ) ) ;
#10485=ORIENTED_EDGE ( 'NONE', *, *, #66526, .F. ) ;
#10612=ORIENTED_EDGE ( 'NONE', *, *, #71566, .T. ) ;
#10618=CIRCLE ( 'NONE', #73768, 24.00000000000000000 ) ;
#10775=ORIENTED_EDGE ( 'NONE', *, *, #22983, .T. ) ;
#10807=CARTESIAN_POINT ( 'NONE',  ( 1.999999999999999112, 18.50000000000000000, 0.000000000000000000 ) ) ;
#10834=AXIS2_PLACEMENT_3D ( 'NONE', #48544, #34805, #33802 ) ;
#10844=DIRECTION ( 'NONE',  ( -1.000000000000000000, 0.000000000000000000, -0.000000000000000000 ) ) ;
#11098=CARTESIAN_POINT ( 'NONE',  ( 10.11708146329084457, 0.6683258531633596844, 18.35000000000000142 ) ) ;
#11154=EDGE_CURVE ( 'NONE', #37020, #72403, #55866, .T. ) ;
#11174=CIRCLE ( 'NONE', #67897, 24.00000000000000000 ) ;
#11270=EDGE_LOOP ( 'NONE', ( #7209, #46255, #25584, #28137 ) ) ;
#11423=ORIENTED_EDGE ( 'NONE', *, *, #94242, .F. ) ;
#11458=CYLINDRICAL_SURFACE ( 'NONE', #47499, 24.00000000000000000 ) ;
#11514=DIRECTION ( 'NONE',  ( 0.000000000000000000, 0.000000000000000000, 1.000000000000000000 ) ) ;
#11548=DIRECTION ( 'NONE',  ( 0.000000000000000000, 0.000000000000000000, 1.000000000000000000 ) ) ;
#11577=DIRECTION ( 'NONE',  ( -1.000000000000000000, -0.000000000000000000, -0.000000000000000000 ) ) ;
#11720=EDGE_CURVE ( 'NONE', #29710, #647, #95802, .T. ) ;
#11793=VERTEX_POINT ( 'NONE', #28789 ) ;
#11816=CARTESIAN_POINT ( 'NONE',  ( 5.550000000000004263, -2.000000000000001776, 19.19609335255483984 ) ) ;
#11831=ORIENTED_EDGE ( 'NONE', *, *, #12988, .T. ) ;
#11985=CARTESIAN_POINT ( 'NONE',  ( 12.92500000000000249, 14.50000000000000000, 24.00000000000000000 ) ) ;
#11986=ORIENTED_EDGE ( 'NONE', *, *, #11720, .T. ) ;
#12094=DIRECTION ( 'NONE',  ( 0.000000000000000000, 0.000000000000000000, -1.000000000000000000 ) ) ;
#12107=CARTESIAN_POINT ( 'NONE',  ( 16.30000000000000071, 0.000000000000000000, 21.89999999999999858 ) ) ;
#12154=DIRECTION ( 'NONE',  ( 1.387778780781445429E-16, -1.000000000000000000, 0.000000000000000000 ) ) ;
#12228=VERTEX_POINT ( 'NONE', #57640 ) ;
#12339=CYLINDRICAL_SURFACE ( 'NONE', #71988, 21.89999999999999858 ) ;
#12400=CARTESIAN_POINT ( 'NONE',  ( 3.675000000000002487, 14.49999999999999822, 24.00000000000000000 ) ) ;
#12540=AXIS2_PLACEMENT_3D ( 'NONE', #91652, #16023, #100242 ) ;
#12793=ORIENTED_EDGE ( 'NONE', *, *, #82545, .F. ) ;
#12895=FACE_OUTER_BOUND ( 'NONE', #65736, .T. ) ;
#12988=EDGE_CURVE ( 'NONE', #68362, #20017, #26937, .T. ) ;
#13178=VECTOR ( 'NONE', #55000, 1000.000000000000000 ) ;
#13246=DIRECTION ( 'NONE',  ( -1.000000000000000000, -0.000000000000000000, -0.000000000000000000 ) ) ;
#13292=AXIS2_PLACEMENT_3D ( 'NONE', #21795, #76089, #5590 ) ;
#13327=CARTESIAN_POINT ( 'NONE',  ( -5.366453405989236813, 0.000000000000000000, 0.000000000000000000 ) ) ;
#13353=ADVANCED_FACE ( 'NONE', ( #35314 ), #82469, .T. ) ;
#13384=DIRECTION ( 'NONE',  ( -1.000000000000000000, -0.000000000000000000, -0.000000000000000000 ) ) ;
#13444=CARTESIAN_POINT ( 'NONE',  ( 0.6000000000000007550, 0.000000000000000000, 21.89999999999999858 ) ) ;
#13589=CARTESIAN_POINT ( 'NONE',  ( -5.366453405989236813, 2.363568322354391830E-15, -19.30000000000000071 ) ) ;
#13636=ORIENTED_EDGE ( 'NONE', *, *, #14840, .T. ) ;
#13644=PLANE ( 'NONE',  #63031 ) ;
#13752=CARTESIAN_POINT ( 'NONE',  ( -5.366453405989236813, 2.681976490132703452E-15, -21.89999999999999858 ) ) ;
#13780=ORIENTED_EDGE ( 'NONE', *, *, #51042, .F. ) ;
#13852=LINE ( 'NONE', #92470, #50273 ) ;
#13891=AXIS2_PLACEMENT_3D ( 'NONE', #20937, #22422, #84331 ) ;
#13917=EDGE_CURVE ( 'NONE', #2943, #48981, #76706, .T. ) ;
#13972=EDGE_CURVE ( 'NONE', #36478, #29598, #26875, .T. ) ;
#13998=AXIS2_PLACEMENT_3D ( 'NONE', #51804, #35582, #89857 ) ;
#14066=AXIS2_PLACEMENT_3D ( 'NONE', #6410, #36860, #7390 ) ;
#14070=ORIENTED_EDGE ( 'NONE', *, *, #39641, .F. ) ;
#14083=LINE ( 'NONE', #85103, #77004 ) ;
#14107=ORIENTED_EDGE ( 'NONE', *, *, #57554, .T. ) ;
#14367=EDGE_LOOP ( 'NONE', ( #96548, #78755, #11986, #63475 ) ) ;
#14511=LINE ( 'NONE', #61707, #56990 ) ;
#14547=CYLINDRICAL_SURFACE ( 'NONE', #84131, 18.35000000000000142 ) ;
#14597=ORIENTED_EDGE ( 'NONE', *, *, #8933, .T. ) ;
#14631=CARTESIAN_POINT ( 'NONE',  ( 16.00000000000000000, 0.000000000000000000, 0.000000000000000000 ) ) ;
#14632=CARTESIAN_POINT ( 'NONE',  ( 1.600000000000000755, 0.000000000000000000, 24.00000000000000000 ) ) ;
#14795=CARTESIAN_POINT ( 'NONE',  ( 12.92500000000000249, 14.50000000000000000, 11.24599928863594300 ) ) ;
#14840=EDGE_CURVE ( 'NONE', #1763, #38912, #14083, .T. ) ;
#14912=CARTESIAN_POINT ( 'NONE',  ( 10.11704143035998271, 0.6681657214399121525, 19.30000000000000071 ) ) ;
#15023=ORIENTED_EDGE ( 'NONE', *, *, #7045, .F. ) ;
#15030=CARTESIAN_POINT ( 'NONE',  ( 15.00000000000000355, 19.30000000000000071, 0.000000000000000000 ) ) ;
#15080=EDGE_CURVE ( 'NONE', #41466, #11793, #24655, .T. ) ;
#15137=ORIENTED_EDGE ( 'NONE', *, *, #49814, .T. ) ;
#15202=DIRECTION ( 'NONE',  ( -1.000000000000000000, -0.000000000000000000, -0.000000000000000000 ) ) ;
#15321=FACE_BOUND ( 'NONE', #21067, .T. ) ;
#15336=ORIENTED_EDGE ( 'NONE', *, *, #73622, .T. ) ;
#15448=CIRCLE ( 'NONE', #86735, 19.30000000000000071 ) ;
#15521=CIRCLE ( 'NONE', #46313, 18.50000000000000000 ) ;
#15535=DIRECTION ( 'NONE',  ( -1.000000000000000000, 0.000000000000000000, -0.000000000000000000 ) ) ;
#15569=FACE_OUTER_BOUND ( 'NONE', #84748, .T. ) ;
#15581=VERTEX_POINT ( 'NONE', #11816 ) ;
#15915=LINE ( 'NONE', #70714, #13178 ) ;
#15931=FACE_BOUND ( 'NONE', #9524, .T. ) ;
#16014=FACE_OUTER_BOUND ( 'NONE', #10405, .T. ) ;
#16016=DIRECTION ( 'NONE',  ( -1.000000000000000000, -3.504491870660219321E-16, 0.000000000000000000 ) ) ;
#16023=DIRECTION ( 'NONE',  ( -1.000000000000000000, -0.000000000000000000, -0.000000000000000000 ) ) ;
#16427=DIRECTION ( 'NONE',  ( -0.000000000000000000, 0.000000000000000000, 1.000000000000000000 ) ) ;
#16597=DIRECTION ( 'NONE',  ( -1.000000000000000000, -0.000000000000000000, -0.000000000000000000 ) ) ;
#16663=FACE_OUTER_BOUND ( 'NONE', #31196, .T. ) ;
#16667=CIRCLE ( 'NONE', #99305, 4.450000000000000178 ) ;
#16687=ADVANCED_FACE ( 'NONE', ( #15569 ), #45540, .T. ) ;
#16697=EDGE_CURVE ( 'NONE', #63151, #66316, #32301, .T. ) ;
#16699=AXIS2_PLACEMENT_3D ( 'NONE', #46207, #77140, #6640 ) ;
#16761=( BOUNDED_CURVE ( )  B_SPLINE_CURVE ( 3, ( #32396, #33386, #49141, #64879 ),
 .UNSPECIFIED., .F., .F. ) 
 B_SPLINE_CURVE_WITH_KNOTS ( ( 4, 4 ),
 ( 4.712388980384689674, 4.821597757366586912 ),
 .UNSPECIFIED. ) 
 CURVE ( )  GEOMETRIC_REPRESENTATION_ITEM ( )  RATIONAL_B_SPLINE_CURVE ( ( 1.000000000000000000, 0.9990063671772055898, 0.9990063671772055898, 1.000000000000000000 ) ) 
 REPRESENTATION_ITEM ( '' )  );
#16786=DIRECTION ( 'NONE',  ( -1.000000000000000000, -0.000000000000000000, -0.000000000000000000 ) ) ;
#16806=VECTOR ( 'NONE', #27784, 1000.000000000000000 ) ;
#17006=DIRECTION ( 'NONE',  ( 0.000000000000000000, 0.000000000000000000, 1.000000000000000000 ) ) ;
#17016=DIRECTION ( 'NONE',  ( 0.000000000000000000, 0.000000000000000000, 1.000000000000000000 ) ) ;
#17019=ORIENTED_EDGE ( 'NONE', *, *, #5097, .F. ) ;
#17032=CARTESIAN_POINT ( 'NONE',  ( 5.550000000000006040, -14.50000000000000178, 12.73734666247252711 ) ) ;
#17181=CARTESIAN_POINT ( 'NONE',  ( 6.817081463290844745, -0.6683258531633596844, 18.35000000000000142 ) ) ;
#17518=ORIENTED_EDGE ( 'NONE', *, *, #82545, .T. ) ;
#17690=EDGE_CURVE ( 'NONE', #48981, #56729, #98232, .T. ) ;
#17716=CARTESIAN_POINT ( 'NONE',  ( 10.45000000000000462, 1.999999999999998668, 18.24068255301867936 ) ) ;
#17746=PLANE ( 'NONE',  #80223 ) ;
#17897=VERTEX_POINT ( 'NONE', #73500 ) ;
#17934=DIRECTION ( 'NONE',  ( -1.000000000000000000, -0.000000000000000000, -0.000000000000000000 ) ) ;
#18095=CYLINDRICAL_SURFACE ( 'NONE', #57849, 6.099999999999999645 ) ;
#18169=DIRECTION ( 'NONE',  ( 0.000000000000000000, 0.000000000000000000, 1.000000000000000000 ) ) ;
#18309=LINE ( 'NONE', #3594, #3226 ) ;
#18356=ORIENTED_EDGE ( 'NONE', *, *, #97462, .F. ) ;
#18459=CARTESIAN_POINT ( 'NONE',  ( 16.00000000000000000, 0.000000000000000000, 0.000000000000000000 ) ) ;
#18498=EDGE_LOOP ( 'NONE', ( #50860, #5399, #52475, #30917 ) ) ;
#18624=CARTESIAN_POINT ( 'NONE',  ( 3.300000000000006040, 0.000000000000000000, 0.000000000000000000 ) ) ;
#18639=LINE ( 'NONE', #32881, #323 ) ;
#18644=DIRECTION ( 'NONE',  ( 0.000000000000000000, 0.000000000000000000, -1.000000000000000000 ) ) ;
#18722=CARTESIAN_POINT ( 'NONE',  ( 6.482918536709166624, 0.6683258531633530231, 18.35000000000000142 ) ) ;
#18985=AXIS2_PLACEMENT_3D ( 'NONE', #42141, #4061, #34011 ) ;
#18995=VERTEX_POINT ( 'NONE', #30547 ) ;
#19018=EDGE_LOOP ( 'NONE', ( #56713, #90135, #26852, #5761 ) ) ;
#19046=PRODUCT_DEFINITION ( 'UNKNOWN', '', #63621, #19561 ) ;
#19260=CARTESIAN_POINT ( 'NONE',  ( 0.000000000000000000, 0.000000000000000000, 0.000000000000000000 ) ) ;
#19312=DIRECTION ( 'NONE',  ( -1.000000000000000000, -0.000000000000000000, -0.000000000000000000 ) ) ;
#19321=DIRECTION ( 'NONE',  ( 0.9701425001453318764, 0.2425356250363331356, 0.000000000000000000 ) ) ;
#19496=CIRCLE ( 'NONE', #47110, 6.099999999999999645 ) ;
#19561=DESIGN_CONTEXT ( 'detailed design', #68626, 'design' ) ;
#19576=ORIENTED_EDGE ( 'NONE', *, *, #74142, .F. ) ;
#19880=FACE_OUTER_BOUND ( 'NONE', #19018, .T. ) ;
#19970=ADVANCED_FACE ( 'NONE', ( #50545 ), #18095, .T. ) ;
#20017=VERTEX_POINT ( 'NONE', #4381 ) ;
#20020=PLANE ( 'NONE',  #93483 ) ;
#20245=VERTEX_POINT ( 'NONE', #65672 ) ;
#20277=LINE ( 'NONE', #43636, #34277 ) ;
#20279=ORIENTED_EDGE ( 'NONE', *, *, #76901, .T. ) ;
#20353=EDGE_LOOP ( 'NONE', ( #66952, #8891, #66302, #27746 ) ) ;
#20376=AXIS2_PLACEMENT_3D ( 'NONE', #68952, #77546, #94280 ) ;
#20527=EDGE_LOOP ( 'NONE', ( #4263, #2428 ) ) ;
#20703=VERTEX_POINT ( 'NONE', #12107 ) ;
#20848=EDGE_CURVE ( 'NONE', #7941, #66316, #100311, .T. ) ;
#20880=ORIENTED_EDGE ( 'NONE', *, *, #62740, .F. ) ;
#20937=CARTESIAN_POINT ( 'NONE',  ( 5.550000000000004263, 0.000000000000000000, 0.000000000000000000 ) ) ;
#21067=EDGE_LOOP ( 'NONE', ( #28742, #22506 ) ) ;
#21200=CARTESIAN_POINT ( 'NONE',  ( -5.366453405989236813, 5.449678256205721784E-16, -4.450000000000000178 ) ) ;
#21214=DIRECTION ( 'NONE',  ( 0.000000000000000000, 0.000000000000000000, 1.000000000000000000 ) ) ;
#21533=CARTESIAN_POINT ( 'NONE',  ( 11.05000000000000426, -2.000000000000000888, 18.24068255301867936 ) ) ;
#21562=DIRECTION ( 'NONE',  ( 0.000000000000000000, 0.000000000000000000, 1.000000000000000000 ) ) ;
#21579=VERTEX_POINT ( 'NONE', #81390 ) ;
#21627=DIRECTION ( 'NONE',  ( 0.000000000000000000, 0.000000000000000000, 1.000000000000000000 ) ) ;
#21735=CARTESIAN_POINT ( 'NONE',  ( 0.000000000000000000, 7.470345474798854293E-16, -6.099999999999999645 ) ) ;
#21795=CARTESIAN_POINT ( 'NONE',  ( 12.92500000000000426, 0.000000000000000000, 0.000000000000000000 ) ) ;
#21940=VECTOR ( 'NONE', #89609, 1000.000000000000000 ) ;
#22061=ORIENTED_EDGE ( 'NONE', *, *, #27228, .T. ) ;
#22079=ORIENTED_EDGE ( 'NONE', *, *, #62272, .F. ) ;
#22097=ORIENTED_EDGE ( 'NONE', *, *, #88021, .T. ) ;
#22170=CARTESIAN_POINT ( 'NONE',  ( 0.3000000000000007661, 2.265596578422603396E-15, -18.50000000000000000 ) ) ;
#22288=ORIENTED_EDGE ( 'NONE', *, *, #649, .F. ) ;
#22296=EDGE_CURVE ( 'NONE', #38301, #85731, #27, .T. ) ;
#22422=DIRECTION ( 'NONE',  ( -1.000000000000000000, -1.387778780781445429E-16, -0.000000000000000000 ) ) ;
#22446=ORIENTED_EDGE ( 'NONE', *, *, #84248, .F. ) ;
#22506=ORIENTED_EDGE ( 'NONE', *, *, #54041, .F. ) ;
#22510=DIRECTION ( 'NONE',  ( -1.000000000000000000, -0.000000000000000000, -0.000000000000000000 ) ) ;
#22586=VECTOR ( 'NONE', #27720, 1000.000000000000000 ) ;
#22631=DIRECTION ( 'NONE',  ( 1.000000000000000000, 0.000000000000000000, 0.000000000000000000 ) ) ;
#22715=DIRECTION ( 'NONE',  ( -1.000000000000000000, -0.000000000000000000, -0.000000000000000000 ) ) ;
#22799=ORIENTED_EDGE ( 'NONE', *, *, #41439, .F. ) ;
#22844=ORIENTED_EDGE ( 'NONE', *, *, #57554, .F. ) ;
#22915=FACE_OUTER_BOUND ( 'NONE', #20527, .T. ) ;
#22983=EDGE_CURVE ( 'NONE', #38301, #37020, #4384, .T. ) ;
#23143=CYLINDRICAL_SURFACE ( 'NONE', #68502, 21.89999999999999858 ) ;
#23256=ORIENTED_EDGE ( 'NONE', *, *, #49670, .F. ) ;
#23303=EDGE_CURVE ( 'NONE', #42203, #38912, #72252, .T. ) ;
#23363=DIRECTION ( 'NONE',  ( -1.000000000000000000, -0.000000000000000000, -0.000000000000000000 ) ) ;
#23386=LINE ( 'NONE', #77677, #89535 ) ;
#23533=UNCERTAINTY_MEASURE_WITH_UNIT (LENGTH_MEASURE( 1.000000000000000082E-05 ), #61271, 'distance_accuracy_value', 'NONE');
#23543=ORIENTED_EDGE ( 'NONE', *, *, #30441, .F. ) ;
#23734=ORIENTED_EDGE ( 'NONE', *, *, #81996, .T. ) ;
#23791=LINE ( 'NONE', #40026, #69038 ) ;
#23808=FACE_BOUND ( 'NONE', #86633, .T. ) ;
#23943=VECTOR ( 'NONE', #48617, 1000.000000000000000 ) ;
#24122=CARTESIAN_POINT ( 'NONE',  ( 6.650000000000004796, 0.000000000000000000, 18.35000000000000142 ) ) ;
#24284=CARTESIAN_POINT ( 'NONE',  ( -5.366453405989236813, 0.000000000000000000, 0.000000000000000000 ) ) ;
#24308=CARTESIAN_POINT ( 'NONE',  ( 15.00000000000000533, 0.000000000000000000, 0.000000000000000000 ) ) ;
#24655=LINE ( 'NONE', #77435, #91567 ) ;
#24706=ORIENTED_EDGE ( 'NONE', *, *, #6192, .F. ) ;
#24781=AXIS2_PLACEMENT_3D ( 'NONE', #29876, #98884, #45120 ) ;
#24816=DIRECTION ( 'NONE',  ( -1.000000000000000000, -0.000000000000000000, -0.000000000000000000 ) ) ;
#24837=CIRCLE ( 'NONE', #68593, 18.50000000000000000 ) ;
#24851=VERTEX_POINT ( 'NONE', #74160 ) ;
#24854=DIRECTION ( 'NONE',  ( 1.000000000000000000, 0.000000000000000000, 0.000000000000000000 ) ) ;
#24864=ORIENTED_EDGE ( 'NONE', *, *, #58968, .T. ) ;
#25141=DIRECTION ( 'NONE',  ( -1.000000000000000000, -0.000000000000000000, -0.000000000000000000 ) ) ;
#25422=VECTOR ( 'NONE', #93510, 1000.000000000000000 ) ;
#25446=CIRCLE ( 'NONE', #14066, 18.50000000000000000 ) ;
#25522=CARTESIAN_POINT ( 'NONE',  ( 0.3000000000000007661, 0.000000000000000000, 21.89999999999999858 ) ) ;
#25566=DIRECTION ( 'NONE',  ( 0.000000000000000000, 0.000000000000000000, 1.000000000000000000 ) ) ;
#25584=ORIENTED_EDGE ( 'NONE', *, *, #13917, .T. ) ;
#25585=DIRECTION ( 'NONE',  ( 0.000000000000000000, 0.000000000000000000, 1.000000000000000000 ) ) ;
#25600=ORIENTED_EDGE ( 'NONE', *, *, #38542, .F. ) ;
#25633=ORIENTED_EDGE ( 'NONE', *, *, #3292, .T. ) ;
#25757=CARTESIAN_POINT ( 'NONE',  ( 16.30000000000000071, 0.000000000000000000, 0.000000000000000000 ) ) ;
#25815=AXIS2_PLACEMENT_3D ( 'NONE', #55801, #78596, #9607 ) ;
#25834=ORIENTED_EDGE ( 'NONE', *, *, #52682, .F. ) ;
#26033=CYLINDRICAL_SURFACE ( 'NONE', #45646, 18.50000000000000000 ) ;
#26040=DIRECTION ( 'NONE',  ( -1.000000000000000000, -0.000000000000000000, -0.000000000000000000 ) ) ;
#26208=DIRECTION ( 'NONE',  ( -1.000000000000000000, -0.000000000000000000, -0.000000000000000000 ) ) ;
#26269=FACE_BOUND ( 'NONE', #54488, .T. ) ;
#26284=CARTESIAN_POINT ( 'NONE',  ( 6.650000000000004796, 0.000000000000000000, 19.30000000000000071 ) ) ;
#26348=DIRECTION ( 'NONE',  ( -1.000000000000000000, 0.000000000000000000, -0.000000000000000000 ) ) ;
#26755=ADVANCED_FACE ( 'NONE', ( #65469 ), #96888, .T. ) ;
#26812=CARTESIAN_POINT ( 'NONE',  ( 9.950000000000006395, 0.000000000000000000, 18.35000000000000142 ) ) ;
#26852=ORIENTED_EDGE ( 'NONE', *, *, #81984, .F. ) ;
#26875=CIRCLE ( 'NONE', #13891, 18.35000000000000142 ) ;
#26937=LINE ( 'NONE', #88847, #83505 ) ;
#27178=PRODUCT ( 'Spool_Varsay\X2\0131\X0\lan', 'Spool_Varsay\X2\0131\X0\lan', '', ( #85309 ) ) ;
#27190=CARTESIAN_POINT ( 'NONE',  ( -5.366453405989236813, 0.000000000000000000, 0.000000000000000000 ) ) ;
#27228=EDGE_CURVE ( 'NONE', #72403, #91284, #65357, .T. ) ;
#27325=CARTESIAN_POINT ( 'NONE',  ( 1.999999999999998224, 0.000000000000000000, 18.50000000000000000 ) ) ;
#27389=DIRECTION ( 'NONE',  ( 0.000000000000000000, 0.000000000000000000, 1.000000000000000000 ) ) ;
#27421=CARTESIAN_POINT ( 'NONE',  ( 0.6000000000000007550, 0.000000000000000000, 0.000000000000000000 ) ) ;
#27435=ADVANCED_FACE ( 'NONE', ( #16014 ), #77405, .T. ) ;
#27720=DIRECTION ( 'NONE',  ( 0.000000000000000000, 0.000000000000000000, -1.000000000000000000 ) ) ;
#27746=ORIENTED_EDGE ( 'NONE', *, *, #8933, .F. ) ;
#27784=DIRECTION ( 'NONE',  ( -1.000000000000000000, -0.000000000000000000, -0.000000000000000000 ) ) ;
#27789=ADVANCED_FACE ( 'NONE', ( #12895 ), #20020, .T. ) ;
#27957=AXIS2_PLACEMENT_3D ( 'NONE', #27421, #66006, #33528 ) ;
#28030=EDGE_CURVE ( 'NONE', #7941, #58804, #672, .T. ) ;
#28035=AXIS2_PLACEMENT_3D ( 'NONE', #2722, #26040, #80330 ) ;
#28137=ORIENTED_EDGE ( 'NONE', *, *, #17690, .T. ) ;
#28191=CARTESIAN_POINT ( 'NONE',  ( -5.366453405989236813, 0.000000000000000000, 0.000000000000000000 ) ) ;
#28221=AXIS2_PLACEMENT_3D ( 'NONE', #96021, #4178, #97018 ) ;
#28241=DIRECTION ( 'NONE',  ( -1.000000000000000000, -0.000000000000000000, -0.000000000000000000 ) ) ;
#28337=CARTESIAN_POINT ( 'NONE',  ( 6.150000000000003908, 1.999999999999998224, 18.24068255301868291 ) ) ;
#28358=AXIS2_PLACEMENT_3D ( 'NONE', #55183, #31321, #62291 ) ;
#28379=DIRECTION ( 'NONE',  ( -1.000000000000000000, -1.387778780781445429E-16, 0.000000000000000000 ) ) ;
#28683=DIRECTION ( 'NONE',  ( 1.000000000000000000, 1.875376730785737473E-16, 0.000000000000000000 ) ) ;
#28718=CARTESIAN_POINT ( 'NONE',  ( -5.366453405989236813, 1.999999999999998224, 19.19609335255483984 ) ) ;
#28742=ORIENTED_EDGE ( 'NONE', *, *, #17690, .F. ) ;
#28789=CARTESIAN_POINT ( 'NONE',  ( 9.450000000000002842, -2.000000000000001332, 19.19609335255483629 ) ) ;
#29328=ORIENTED_EDGE ( 'NONE', *, *, #62272, .T. ) ;
#29431=ADVANCED_BREP_SHAPE_REPRESENTATION ( '', ( #43720, #37391 ), #45585 ) ;
#29456=ORIENTED_EDGE ( 'NONE', *, *, #14840, .F. ) ;
#29598=VERTEX_POINT ( 'NONE', #72107 ) ;
#29710=VERTEX_POINT ( 'NONE', #58379 ) ;
#29735=DIRECTION ( 'NONE',  ( 0.000000000000000000, 0.000000000000000000, 1.000000000000000000 ) ) ;
#29876=CARTESIAN_POINT ( 'NONE',  ( 5.550000000000004263, 0.000000000000000000, 0.000000000000000000 ) ) ;
#30011=CIRCLE ( 'NONE', #85141, 19.30000000000000071 ) ;
#30015=VECTOR ( 'NONE', #96719, 1000.000000000000000 ) ;
#30054=CARTESIAN_POINT ( 'NONE',  ( 16.00000000000000000, 0.000000000000000000, 21.89999999999999858 ) ) ;
#30081=CIRCLE ( 'NONE', #20376, 6.099999999999999645 ) ;
#30141=CARTESIAN_POINT ( 'NONE',  ( 9.950000000000006395, 0.000000000000000000, 19.30000000000000071 ) ) ;
#30246=CYLINDRICAL_SURFACE ( 'NONE', #51948, 18.50000000000000000 ) ;
#30333=ADVANCED_FACE ( 'NONE', ( #60733, #36881 ), #67346, .F. ) ;
#30358=DIRECTION ( 'NONE',  ( -1.000000000000000000, -0.000000000000000000, -0.000000000000000000 ) ) ;
#30410=FACE_OUTER_BOUND ( 'NONE', #20353, .T. ) ;
#30441=EDGE_CURVE ( 'NONE', #67226, #20703, #87712, .T. ) ;
#30462=ORIENTED_EDGE ( 'NONE', *, *, #69834, .F. ) ;
#30481=VERTEX_POINT ( 'NONE', #54609 ) ;
#30547=CARTESIAN_POINT ( 'NONE',  ( 3.300000000000006040, 5.449678256205721784E-16, -4.450000000000000178 ) ) ;
#30626=EDGE_CURVE ( 'NONE', #77342, #36478, #68715, .T. ) ;
#30786=FACE_OUTER_BOUND ( 'NONE', #70548, .T. ) ;
#30796=DIRECTION ( 'NONE',  ( 0.000000000000000000, 0.000000000000000000, 1.000000000000000000 ) ) ;
#30887=CARTESIAN_POINT ( 'NONE',  ( 0.3000000000000007661, 0.000000000000000000, 0.000000000000000000 ) ) ;
#30917=ORIENTED_EDGE ( 'NONE', *, *, #3292, .F. ) ;
#30953=VERTEX_POINT ( 'NONE', #33651 ) ;
#30962=CARTESIAN_POINT ( 'NONE',  ( 1.600000000000000755, 0.000000000000000000, 0.000000000000000000 ) ) ;
#31196=EDGE_LOOP ( 'NONE', ( #84144, #3319, #79414, #13780 ) ) ;
#31236=ORIENTED_EDGE ( 'NONE', *, *, #53424, .F. ) ;
#31295=EDGE_LOOP ( 'NONE', ( #69690, #23734, #86967, #76483, #4777, #59819 ) ) ;
#31304=CARTESIAN_POINT ( 'NONE',  ( 3.300000000000006040, 0.000000000000000000, 4.450000000000000178 ) ) ;
#31321=DIRECTION ( 'NONE',  ( -1.000000000000000000, -0.000000000000000000, -0.000000000000000000 ) ) ;
#31517=ORIENTED_EDGE ( 'NONE', *, *, #37860, .F. ) ;
#31537=CIRCLE ( 'NONE', #67268, 24.00000000000000000 ) ;
#31619=CARTESIAN_POINT ( 'NONE',  ( -5.366453405989236813, 0.000000000000000000, 18.35000000000000142 ) ) ;
#31891=VECTOR ( 'NONE', #2843, 1000.000000000000000 ) ;
#31970=FACE_OUTER_BOUND ( 'NONE', #4399, .T. ) ;
#32301=LINE ( 'NONE', #9966, #36458 ) ;
#32317=VECTOR ( 'NONE', #12094, 1000.000000000000000 ) ;
#32396=CARTESIAN_POINT ( 'NONE',  ( 9.950000000000006395, 0.000000000000000000, 18.35000000000000142 ) ) ;
#32858=AXIS2_PLACEMENT_3D ( 'NONE', #59601, #44375, #59106 ) ;
#32881=CARTESIAN_POINT ( 'NONE',  ( 5.550000000000004263, -2.000000000000001776, 24.00000000000000000 ) ) ;
#32947=EDGE_CURVE ( 'NONE', #86308, #69912, #45690, .T. ) ;
#32973=AXIS2_PLACEMENT_3D ( 'NONE', #38772, #47902, #16427 ) ;
#32996=DIRECTION ( 'NONE',  ( -1.000000000000000000, -0.000000000000000000, -0.000000000000000000 ) ) ;
#32997=ORIENTED_EDGE ( 'NONE', *, *, #65508, .T. ) ;
#33213=CARTESIAN_POINT ( 'NONE',  ( 9.950000000000006395, 0.000000000000000000, 19.30000000000000071 ) ) ;
#33280=CARTESIAN_POINT ( 'NONE',  ( 3.675000000000004707, 1.999999999999998224, 19.19609335255483984 ) ) ;
#33386=CARTESIAN_POINT ( 'NONE',  ( 9.782918536709168222, -0.6683258531633530231, 18.35000000000000142 ) ) ;
#33413=AXIS2_PLACEMENT_3D ( 'NONE', #49678, #24816, #86224 ) ;
#33416=ORIENTED_EDGE ( 'NONE', *, *, #28030, .F. ) ;
#33528=DIRECTION ( 'NONE',  ( 0.000000000000000000, 0.000000000000000000, 1.000000000000000000 ) ) ;
#33614=ADVANCED_FACE ( 'NONE', ( #74236 ), #65654, .T. ) ;
#33642=ORIENTED_EDGE ( 'NONE', *, *, #69992, .T. ) ;
#33651=CARTESIAN_POINT ( 'NONE',  ( 0.000000000000000000, 0.000000000000000000, 6.099999999999999645 ) ) ;
#33704=ORIENTED_EDGE ( 'NONE', *, *, #30626, .T. ) ;
#33802=DIRECTION ( 'NONE',  ( -1.797640907747986603E-16, 1.000000000000000000, 0.000000000000000000 ) ) ;
#33810=CARTESIAN_POINT ( 'NONE',  ( 1.600000000000000755, 2.939152317953647894E-15, -24.00000000000000000 ) ) ;
#33833=ORIENTED_EDGE ( 'NONE', *, *, #10258, .F. ) ;
#33919=VECTOR ( 'NONE', #82492, 1000.000000000000000 ) ;
#34011=DIRECTION ( 'NONE',  ( 1.000000000000000000, 2.710505431213760099E-16, 0.000000000000000000 ) ) ;
#34045=FACE_OUTER_BOUND ( 'NONE', #99950, .T. ) ;
#34277=VECTOR ( 'NONE', #50755, 1000.000000000000000 ) ;
#34339=EDGE_LOOP ( 'NONE', ( #97898, #91225, #93829, #51063, #44953, #67946, #80666, #90547, #40071, #45959, #80166, #10242 ) ) ;
#34736=ORIENTED_EDGE ( 'NONE', *, *, #57032, .T. ) ;
#34754=DIRECTION ( 'NONE',  ( -1.734723475976806848E-16, 1.000000000000000000, 0.000000000000000000 ) ) ;
#34805=DIRECTION ( 'NONE',  ( 1.000000000000000000, 1.734723475976806848E-16, 0.000000000000000000 ) ) ;
#34910=DIRECTION ( 'NONE',  ( 1.000000000000000000, 0.000000000000000000, 0.000000000000000000 ) ) ;
#35008=EDGE_CURVE ( 'NONE', #38489, #60035, #60057, .T. ) ;
#35026=CIRCLE ( 'NONE', #91714, 18.35000000000000142 ) ;
#35247=EDGE_CURVE ( 'NONE', #17897, #20245, #13852, .T. ) ;
#35314=FACE_OUTER_BOUND ( 'NONE', #34339, .T. ) ;
#35582=DIRECTION ( 'NONE',  ( -1.000000000000000000, -0.000000000000000000, -0.000000000000000000 ) ) ;
#35680=CARTESIAN_POINT ( 'NONE',  ( 12.92500000000000249, 14.50000000000000000, 24.00000000000000000 ) ) ;
#35734=ORIENTED_EDGE ( 'NONE', *, *, #78526, .T. ) ;
#36046=ORIENTED_EDGE ( 'NONE', *, *, #63449, .F. ) ;
#36218=VECTOR ( 'NONE', #11577, 1000.000000000000000 ) ;
#36333=VERTEX_POINT ( 'NONE', #40721 ) ;
#36344=DIRECTION ( 'NONE',  ( -1.000000000000000000, -0.000000000000000000, -0.000000000000000000 ) ) ;
#36428=AXIS2_PLACEMENT_3D ( 'NONE', #53998, #38749, #100125 ) ;
#36458=VECTOR ( 'NONE', #71379, 1000.000000000000000 ) ;
#36478=VERTEX_POINT ( 'NONE', #54565 ) ;
#36529=CARTESIAN_POINT ( 'NONE',  ( 6.650000000000004796, 0.000000000000000000, 19.30000000000000071 ) ) ;
#36535=CIRCLE ( 'NONE', #912, 6.099999999999999645 ) ;
#36538=AXIS2_PLACEMENT_3D ( 'NONE', #67078, #67570, #59960 ) ;
#36591=DIRECTION ( 'NONE',  ( 0.000000000000000000, 0.000000000000000000, 1.000000000000000000 ) ) ;
#36846=DIRECTION ( 'NONE',  ( 0.000000000000000000, 0.000000000000000000, 1.000000000000000000 ) ) ;
#36860=DIRECTION ( 'NONE',  ( -1.000000000000000000, -0.000000000000000000, -0.000000000000000000 ) ) ;
#36881=FACE_OUTER_BOUND ( 'NONE', #69990, .T. ) ;
#36893=DIRECTION ( 'NONE',  ( -1.000000000000000000, -0.000000000000000000, -0.000000000000000000 ) ) ;
#36895=DIRECTION ( 'NONE',  ( -1.000000000000000000, -0.000000000000000000, -0.000000000000000000 ) ) ;
#37020=VERTEX_POINT ( 'NONE', #73669 ) ;
#37050=DIRECTION ( 'NONE',  ( -1.000000000000000000, -0.000000000000000000, -0.000000000000000000 ) ) ;
#37231=CARTESIAN_POINT ( 'NONE',  ( 9.950000000000006395, 0.000000000000000000, 19.30000000000000071 ) ) ;
#37326=EDGE_CURVE ( 'NONE', #17897, #44273, #83014, .T. ) ;
#37391=AXIS2_PLACEMENT_3D ( 'NONE', #1533, #63447, #24854 ) ;
#37516=( BOUNDED_CURVE ( )  B_SPLINE_CURVE ( 3, ( #52266, #99422, #83701, #36529 ),
 .UNSPECIFIED., .F., .T. ) 
 B_SPLINE_CURVE_WITH_KNOTS ( ( 4, 4 ),
 ( 1.466983014708610034, 1.570796326794896558 ),
 .UNSPECIFIED. ) 
 CURVE ( )  GEOMETRIC_REPRESENTATION_ITEM ( )  RATIONAL_B_SPLINE_CURVE ( ( 1.000000000000000000, 0.9991021013140741758, 0.9991021013140741758, 1.000000000000000000 ) ) 
 REPRESENTATION_ITEM ( '' )  );
#37519=ORIENTED_EDGE ( 'NONE', *, *, #78139, .T. ) ;
#37712=EDGE_CURVE ( 'NONE', #38912, #42203, #86352, .T. ) ;
#37860=EDGE_CURVE ( 'NONE', #1763, #24851, #60440, .T. ) ;
#37896=AXIS2_PLACEMENT_3D ( 'NONE', #47000, #15535, #93659 ) ;
#37918=DIRECTION ( 'NONE',  ( 0.000000000000000000, -0.000000000000000000, 1.000000000000000000 ) ) ;
#38099=( BOUNDED_CURVE ( )  B_SPLINE_CURVE ( 3, ( #30141, #14912, #6808, #74820 ),
 .UNSPECIFIED., .F., .F. ) 
 B_SPLINE_CURVE_WITH_KNOTS ( ( 4, 4 ),
 ( 1.570796326794896558, 1.674609638881183082 ),
 .UNSPECIFIED. ) 
 CURVE ( )  GEOMETRIC_REPRESENTATION_ITEM ( )  RATIONAL_B_SPLINE_CURVE ( ( 1.000000000000000000, 0.9991021013140741758, 0.9991021013140741758, 1.000000000000000000 ) ) 
 REPRESENTATION_ITEM ( '' )  );
#38288=DIRECTION ( 'NONE',  ( -1.000000000000000000, -0.000000000000000000, -0.000000000000000000 ) ) ;
#38301=VERTEX_POINT ( 'NONE', #79665 ) ;
#38323=AXIS2_PLACEMENT_3D ( 'NONE', #40147, #71102, #1592 ) ;
#38361=CARTESIAN_POINT ( 'NONE',  ( 12.92500000000000249, 1.999999999999999556, 24.00000000000000000 ) ) ;
#38389=FACE_OUTER_BOUND ( 'NONE', #57684, .T. ) ;
#38399=CARTESIAN_POINT ( 'NONE',  ( 0.000000000000000000, 0.000000000000000000, 0.000000000000000000 ) ) ;
#38419=EDGE_CURVE ( 'NONE', #15581, #76298, #76624, .T. ) ;
#38436=LINE ( 'NONE', #13589, #74418 ) ;
#38461=ORIENTED_EDGE ( 'NONE', *, *, #96068, .T. ) ;
#38489=VERTEX_POINT ( 'NONE', #77538 ) ;
#38542=EDGE_CURVE ( 'NONE', #58804, #20245, #3801, .T. ) ;
#38551=ADVANCED_FACE ( 'NONE', ( #62855 ), #78535, .T. ) ;
#38575=ORIENTED_EDGE ( 'NONE', *, *, #7045, .T. ) ;
#38749=DIRECTION ( 'NONE',  ( -1.000000000000000000, -0.000000000000000000, -0.000000000000000000 ) ) ;
#38772=CARTESIAN_POINT ( 'NONE',  ( 16.00000000000000000, 21.89999999999999858, 0.000000000000000000 ) ) ;
#38905=CARTESIAN_POINT ( 'NONE',  ( -5.366453405989236813, 0.000000000000000000, 0.000000000000000000 ) ) ;
#38912=VERTEX_POINT ( 'NONE', #25522 ) ;
#38954=EDGE_LOOP ( 'NONE', ( #92618, #6920 ) ) ;
#38975=AXIS2_PLACEMENT_3D ( 'NONE', #79551, #88675, #18644 ) ;
#39040=PLANE ( 'NONE',  #46815 ) ;
#39373=AXIS2_PLACEMENT_3D ( 'NONE', #82764, #13246, #36591 ) ;
#39384=FACE_BOUND ( 'NONE', #73276, .T. ) ;
#39505=CARTESIAN_POINT ( 'NONE',  ( 3.675000000000002487, 14.49999999999999822, 12.73734666247253244 ) ) ;
#39545=DIRECTION ( 'NONE',  ( 1.000000000000000000, 0.000000000000000000, 0.000000000000000000 ) ) ;
#39641=EDGE_CURVE ( 'NONE', #66316, #43365, #76549, .T. ) ;
#39867=AXIS2_PLACEMENT_3D ( 'NONE', #24284, #78550, #18169 ) ;
#39945=ORIENTED_EDGE ( 'NONE', *, *, #30441, .T. ) ;
#39948=DIRECTION ( 'NONE',  ( 0.000000000000000000, 0.000000000000000000, 1.000000000000000000 ) ) ;
#39953=CIRCLE ( 'NONE', #10834, 19.30000000000000071 ) ;
#40026=CARTESIAN_POINT ( 'NONE',  ( 12.92500000000000249, 1.999999999999999556, 24.00000000000000000 ) ) ;
#40071=ORIENTED_EDGE ( 'NONE', *, *, #11154, .F. ) ;
#40075=FACE_BOUND ( 'NONE', #60851, .T. ) ;
#40092=ADVANCED_FACE ( 'NONE', ( #92164, #39384 ), #7929, .F. ) ;
#40147=CARTESIAN_POINT ( 'NONE',  ( 16.30000000000000071, 21.89999999999999858, 0.000000000000000000 ) ) ;
#40314=CARTESIAN_POINT ( 'NONE',  ( 0.3000000000000007661, 0.000000000000000000, 0.000000000000000000 ) ) ;
#40323=ORIENTED_EDGE ( 'NONE', *, *, #15080, .F. ) ;
#40553=DIRECTION ( 'NONE',  ( 0.000000000000000000, 0.000000000000000000, -1.000000000000000000 ) ) ;
#40654=FACE_OUTER_BOUND ( 'NONE', #41221, .T. ) ;
#40661=ORIENTED_EDGE ( 'NONE', *, *, #81996, .F. ) ;
#40721=CARTESIAN_POINT ( 'NONE',  ( 1.600000000000000755, 0.000000000000000000, 19.30000000000000071 ) ) ;
#40957=ADVANCED_FACE ( 'NONE', ( #30410 ), #83188, .T. ) ;
#41050=CIRCLE ( 'NONE', #39373, 4.450000000000000178 ) ;
#41221=EDGE_LOOP ( 'NONE', ( #78123, #23543 ) ) ;
#41283=EDGE_LOOP ( 'NONE', ( #44180, #51633, #29328, #30462 ) ) ;
#41418=CARTESIAN_POINT ( 'NONE',  ( 0.000000000000000000, 5.449678256205721784E-16, -4.450000000000000178 ) ) ;
#41439=EDGE_CURVE ( 'NONE', #57039, #20017, #16667, .T. ) ;
#41466=VERTEX_POINT ( 'NONE', #63770 ) ;
#41500=PLANE ( 'NONE',  #38975 ) ;
#41571=CARTESIAN_POINT ( 'NONE',  ( 1.999999999999998224, 2.265596578422603396E-15, -18.50000000000000000 ) ) ;
#41724=ORIENTED_EDGE ( 'NONE', *, *, #2877, .F. ) ;
#41760=DIRECTION ( 'NONE',  ( 0.000000000000000000, 0.000000000000000000, -1.000000000000000000 ) ) ;
#41775=ADVANCED_FACE ( 'NONE', ( #85444, #15931 ), #46897, .F. ) ;
#41812=CARTESIAN_POINT ( 'NONE',  ( 16.00000000000000000, 0.000000000000000000, 0.000000000000000000 ) ) ;
#41818=DIRECTION ( 'NONE',  ( -1.000000000000000000, -0.000000000000000000, -0.000000000000000000 ) ) ;
#41906=LINE ( 'NONE', #72347, #31891 ) ;
#42055=EDGE_LOOP ( 'NONE', ( #31236, #64454, #13636, #3108 ) ) ;
#42112=VECTOR ( 'NONE', #88038, 1000.000000000000000 ) ;
#42141=CARTESIAN_POINT ( 'NONE',  ( 9.450000000000002842, -2.000000000000001332, 24.00000000000000000 ) ) ;
#42175=CARTESIAN_POINT ( 'NONE',  ( -5.366453405989236813, 0.000000000000000000, 0.000000000000000000 ) ) ;
#42203=VERTEX_POINT ( 'NONE', #97773 ) ;
#42473=ORIENTED_EDGE ( 'NONE', *, *, #30626, .F. ) ;
#42571=CIRCLE ( 'NONE', #32858, 21.89999999999999858 ) ;
#42631=AXIS2_PLACEMENT_3D ( 'NONE', #96638, #22715, #46584 ) ;
#42982=VERTEX_POINT ( 'NONE', #71478 ) ;
#43045=DIRECTION ( 'NONE',  ( 0.000000000000000000, 0.000000000000000000, 1.000000000000000000 ) ) ;
#43196=EDGE_CURVE ( 'NONE', #60911, #36333, #50626, .T. ) ;
#43308=DIRECTION ( 'NONE',  ( 0.000000000000000000, 0.000000000000000000, 1.000000000000000000 ) ) ;
#43327=ORIENTED_EDGE ( 'NONE', *, *, #28030, .T. ) ;
#43347=ADVANCED_FACE ( 'NONE', ( #52620 ), #23143, .T. ) ;
#43365=VERTEX_POINT ( 'NONE', #76434 ) ;
#43377=DIRECTION ( 'NONE',  ( 1.000000000000000000, 1.387778780781445429E-16, 0.000000000000000000 ) ) ;
#43636=CARTESIAN_POINT ( 'NONE',  ( -5.366453405989236813, -2.000000000000001776, 18.24068255301867936 ) ) ;
#43720=MANIFOLD_SOLID_BREP ( 'Kes-Ekstr\X2\00fc\X0\zyon1', #58224 ) ;
#43898=DIRECTION ( 'NONE',  ( -1.000000000000000000, -0.000000000000000000, -0.000000000000000000 ) ) ;
#43917=DIRECTION ( 'NONE',  ( -1.000000000000000000, -0.000000000000000000, -0.000000000000000000 ) ) ;
#43964=EDGE_CURVE ( 'NONE', #20017, #57039, #50693, .T. ) ;
#44008=CARTESIAN_POINT ( 'NONE',  ( -5.366453405989236813, 0.000000000000000000, 0.000000000000000000 ) ) ;
#44172=CARTESIAN_POINT ( 'NONE',  ( -5.366453405989236813, 0.000000000000000000, 6.099999999999999645 ) ) ;
#44180=ORIENTED_EDGE ( 'NONE', *, *, #49670, .T. ) ;
#44273=VERTEX_POINT ( 'NONE', #8708 ) ;
#44336=AXIS2_PLACEMENT_3D ( 'NONE', #24308, #78576, #9083 ) ;
#44375=DIRECTION ( 'NONE',  ( -1.000000000000000000, -0.000000000000000000, -0.000000000000000000 ) ) ;
#44436=CARTESIAN_POINT ( 'NONE',  ( -5.366453405989236813, 0.000000000000000000, 24.00000000000000000 ) ) ;
#44628=CARTESIAN_POINT ( 'NONE',  ( -5.366453405989236813, 1.999999999999998224, 18.24068255301867936 ) ) ;
#44679=ORIENTED_EDGE ( 'NONE', *, *, #7319, .F. ) ;
#44835=EDGE_LOOP ( 'NONE', ( #24706, #85970, #96851, #50844 ) ) ;
#44851=CARTESIAN_POINT ( 'NONE',  ( 9.782958569640028301, -0.6681657214399144840, 19.30000000000000071 ) ) ;
#44852=ADVANCED_FACE ( 'NONE', ( #73367 ), #11458, .T. ) ;
#44953=ORIENTED_EDGE ( 'NONE', *, *, #56244, .F. ) ;
#45008=CIRCLE ( 'NONE', #12540, 21.89999999999999858 ) ;
#45120=DIRECTION ( 'NONE',  ( -1.348230680810989829E-16, 1.000000000000000000, 0.000000000000000000 ) ) ;
#45518=DIRECTION ( 'NONE',  ( 0.000000000000000000, 0.000000000000000000, 1.000000000000000000 ) ) ;
#45540=PLANE ( 'NONE',  #5603 ) ;
#45585=( GEOMETRIC_REPRESENTATION_CONTEXT ( 3 ) GLOBAL_UNCERTAINTY_ASSIGNED_CONTEXT ( ( #23533 ) ) GLOBAL_UNIT_ASSIGNED_CONTEXT ( ( #61271, #86084, #53655 ) ) REPRESENTATION_CONTEXT ( 'NONE', 'WORKASPACE' ) );
#45646=AXIS2_PLACEMENT_3D ( 'NONE', #4205, #94543, #57008 ) ;
#45690=CIRCLE ( 'NONE', #13292, 18.35000000000000142 ) ;
#45807=CARTESIAN_POINT ( 'NONE',  ( 16.30000000000000071, 2.681976490132703452E-15, -21.89999999999999858 ) ) ;
#45959=ORIENTED_EDGE ( 'NONE', *, *, #22983, .F. ) ;
#45970=DIRECTION ( 'NONE',  ( -1.000000000000000000, -0.000000000000000000, -0.000000000000000000 ) ) ;
#46071=FACE_OUTER_BOUND ( 'NONE', #48738, .T. ) ;
#46112=DIRECTION ( 'NONE',  ( -1.000000000000000000, -0.000000000000000000, -0.000000000000000000 ) ) ;
#46207=CARTESIAN_POINT ( 'NONE',  ( 10.45000000000000462, 1.999999999999998668, 24.00000000000000000 ) ) ;
#46249=AXIS2_PLACEMENT_3D ( 'NONE', #18624, #28241, #11514 ) ;
#46253=CIRCLE ( 'NONE', #28358, 19.30000000000000071 ) ;
#46255=ORIENTED_EDGE ( 'NONE', *, *, #78526, .F. ) ;
#46313=AXIS2_PLACEMENT_3D ( 'NONE', #30887, #78041, #62350 ) ;
#46476=DIRECTION ( 'NONE',  ( 0.000000000000000000, -0.000000000000000000, 1.000000000000000000 ) ) ;
#46480=DIRECTION ( 'NONE',  ( -3.504491870660219321E-16, 1.000000000000000000, 0.000000000000000000 ) ) ;
#46565=VERTEX_POINT ( 'NONE', #64180 ) ;
#46584=DIRECTION ( 'NONE',  ( 0.000000000000000000, 0.000000000000000000, 1.000000000000000000 ) ) ;
#46815=AXIS2_PLACEMENT_3D ( 'NONE', #9594, #39545, #40553 ) ;
#46897=PLANE ( 'NONE',  #32973 ) ;
#46985=ORIENTED_EDGE ( 'NONE', *, *, #54143, .F. ) ;
#47000=CARTESIAN_POINT ( 'NONE',  ( 1.600000000000000977, 24.00000000000000000, 0.000000000000000000 ) ) ;
#47053=ORIENTED_EDGE ( 'NONE', *, *, #73622, .F. ) ;
#47093=VERTEX_POINT ( 'NONE', #1133 ) ;
#47110=AXIS2_PLACEMENT_3D ( 'NONE', #96791, #95791, #11548 ) ;
#47371=ORIENTED_EDGE ( 'NONE', *, *, #37326, .T. ) ;
#47499=AXIS2_PLACEMENT_3D ( 'NONE', #27190, #51026, #3371 ) ;
#47902=DIRECTION ( 'NONE',  ( -1.000000000000000000, 0.000000000000000000, -0.000000000000000000 ) ) ;
#48315=ADVANCED_FACE ( 'NONE', ( #83761 ), #60945, .T. ) ;
#48332=EDGE_CURVE ( 'NONE', #18995, #68362, #41050, .T. ) ;
#48544=CARTESIAN_POINT ( 'NONE',  ( 3.675000000000004707, 0.000000000000000000, 0.000000000000000000 ) ) ;
#48617=DIRECTION ( 'NONE',  ( -1.000000000000000000, -0.000000000000000000, -0.000000000000000000 ) ) ;
#48655=VERTEX_POINT ( 'NONE', #21735 ) ;
#48682=VERTEX_POINT ( 'NONE', #14632 ) ;
#48685=CARTESIAN_POINT ( 'NONE',  ( 10.28391390014267692, 1.335655600570678558, 18.31352460785937453 ) ) ;
#48738=EDGE_LOOP ( 'NONE', ( #51501, #32997, #33833, #64505 ) ) ;
#48889=FACE_OUTER_BOUND ( 'NONE', #44835, .T. ) ;
#48981=VERTEX_POINT ( 'NONE', #8023 ) ;
#49136=VECTOR ( 'NONE', #5086, 1000.000000000000000 ) ;
#49141=CARTESIAN_POINT ( 'NONE',  ( 9.616086099857337643, -1.335655600570672119, 18.31352460785937097 ) ) ;
#49246=APPLICATION_CONTEXT ( 'configuration controlled 3d designs of mechanical parts and assemblies' ) ;
#49426=DIRECTION ( 'NONE',  ( -1.000000000000000000, -0.000000000000000000, -0.000000000000000000 ) ) ;
#49431=DIRECTION ( 'NONE',  ( 0.000000000000000000, 0.000000000000000000, 1.000000000000000000 ) ) ;
#49498=ORIENTED_EDGE ( 'NONE', *, *, #2877, .T. ) ;
#49519=ADVANCED_FACE ( 'NONE', ( #19880 ), #65102, .T. ) ;
#49665=CIRCLE ( 'NONE', #56186, 18.35000000000000142 ) ;
#49670=EDGE_CURVE ( 'NONE', #60943, #41466, #88135, .T. ) ;
#49678=CARTESIAN_POINT ( 'NONE',  ( 0.3000000000000007661, 0.000000000000000000, 0.000000000000000000 ) ) ;
#49715=VERTEX_POINT ( 'NONE', #65919 ) ;
#49730=EDGE_CURVE ( 'NONE', #18995, #57039, #74986, .T. ) ;
#49814=EDGE_CURVE ( 'NONE', #47093, #91990, #75144, .T. ) ;
#49914=AXIS2_PLACEMENT_3D ( 'NONE', #99736, #76409, #46476 ) ;
#50133=CARTESIAN_POINT ( 'NONE',  ( -5.366453405989236813, 0.000000000000000000, 19.30000000000000071 ) ) ;
#50140=ADVANCED_FACE ( 'NONE', ( #50418 ), #12339, .T. ) ;
#50239=FACE_OUTER_BOUND ( 'NONE', #14367, .T. ) ;
#50273=VECTOR ( 'NONE', #75745, 1000.000000000000000 ) ;
#50292=DIRECTION ( 'NONE',  ( -0.2425356250363331356, 0.9701425001453318764, 0.000000000000000000 ) ) ;
#50418=FACE_OUTER_BOUND ( 'NONE', #96126, .T. ) ;
#50545=FACE_OUTER_BOUND ( 'NONE', #98305, .T. ) ;
#50626=LINE ( 'NONE', #50133, #16806 ) ;
#50674=LINE ( 'NONE', #81620, #32317 ) ;
#50693=CIRCLE ( 'NONE', #57233, 4.450000000000000178 ) ;
#50755=DIRECTION ( 'NONE',  ( 1.000000000000000000, 0.000000000000000000, 0.000000000000000000 ) ) ;
#50844=ORIENTED_EDGE ( 'NONE', *, *, #13917, .F. ) ;
#50860=ORIENTED_EDGE ( 'NONE', *, *, #59697, .T. ) ;
#50955=ORIENTED_EDGE ( 'NONE', *, *, #43196, .T. ) ;
#51026=DIRECTION ( 'NONE',  ( -1.000000000000000000, -0.000000000000000000, -0.000000000000000000 ) ) ;
#51042=EDGE_CURVE ( 'NONE', #89130, #89740, #55831, .T. ) ;
#51063=ORIENTED_EDGE ( 'NONE', *, *, #43196, .F. ) ;
#51339=CYLINDRICAL_SURFACE ( 'NONE', #36538, 24.00000000000000000 ) ;
#51501=ORIENTED_EDGE ( 'NONE', *, *, #67948, .T. ) ;
#51563=LINE ( 'NONE', #28718, #33919 ) ;
#51565=EDGE_LOOP ( 'NONE', ( #928, #80976 ) ) ;
#51633=ORIENTED_EDGE ( 'NONE', *, *, #97033, .T. ) ;
#51692=ORIENTED_EDGE ( 'NONE', *, *, #68448, .F. ) ;
#51804=CARTESIAN_POINT ( 'NONE',  ( -5.366453405989236813, 0.000000000000000000, 0.000000000000000000 ) ) ;
#51851=EDGE_CURVE ( 'NONE', #68549, #48682, #31537, .T. ) ;
#51901=ADVANCED_FACE ( 'NONE', ( #31970 ), #17746, .T. ) ;
#51948=AXIS2_PLACEMENT_3D ( 'NONE', #67840, #74918, #21627 ) ;
#52060=EDGE_LOOP ( 'NONE', ( #35734, #63591 ) ) ;
#52266=CARTESIAN_POINT ( 'NONE',  ( 6.150000000000003908, 1.999999999999998224, 19.19609335255483629 ) ) ;
#52309=ORIENTED_EDGE ( 'NONE', *, *, #32947, .T. ) ;
#52475=ORIENTED_EDGE ( 'NONE', *, *, #52710, .F. ) ;
#52487=EDGE_CURVE ( 'NONE', #68362, #18995, #86667, .T. ) ;
#52497=EDGE_LOOP ( 'NONE', ( #56482, #53395, #11831, #85871 ) ) ;
#52510=LINE ( 'NONE', #6817, #59665 ) ;
#52600=FACE_OUTER_BOUND ( 'NONE', #11270, .T. ) ;
#52620=FACE_OUTER_BOUND ( 'NONE', #60611, .T. ) ;
#52665=EDGE_CURVE ( 'NONE', #36333, #80276, #15448, .T. ) ;
#52682=EDGE_CURVE ( 'NONE', #80276, #36333, #30011, .T. ) ;
#52710=EDGE_CURVE ( 'NONE', #42982, #73818, #10618, .T. ) ;
#53012=CARTESIAN_POINT ( 'NONE',  ( 10.45000000000000462, 1.999999999999998668, 18.24068255301867936 ) ) ;
#53173=DIRECTION ( 'NONE',  ( -1.000000000000000000, -0.000000000000000000, -0.000000000000000000 ) ) ;
#53240=EDGE_CURVE ( 'NONE', #43365, #78758, #68921, .T. ) ;
#53273=VECTOR ( 'NONE', #38288, 1000.000000000000000 ) ;
#53314=DIRECTION ( 'NONE',  ( -1.000000000000000000, -0.000000000000000000, -0.000000000000000000 ) ) ;
#53395=ORIENTED_EDGE ( 'NONE', *, *, #52487, .F. ) ;
#53424=EDGE_CURVE ( 'NONE', #24851, #42203, #58956, .T. ) ;
#53446=ADVANCED_FACE ( 'NONE', ( #68554 ), #51339, .T. ) ;
#53580=CARTESIAN_POINT ( 'NONE',  ( 16.30000000000000071, 0.000000000000000000, 0.000000000000000000 ) ) ;
#53636=DIRECTION ( 'NONE',  ( -1.000000000000000000, -0.000000000000000000, -0.000000000000000000 ) ) ;
#53655=( NAMED_UNIT ( * ) SI_UNIT ( $, .STERADIAN. ) SOLID_ANGLE_UNIT ( ) );
#53761=DIRECTION ( 'NONE',  ( 0.000000000000000000, 0.000000000000000000, -1.000000000000000000 ) ) ;
#53998=CARTESIAN_POINT ( 'NONE',  ( 12.92500000000000426, 0.000000000000000000, 0.000000000000000000 ) ) ;
#54041=EDGE_CURVE ( 'NONE', #56729, #48981, #15521, .T. ) ;
#54089=DIRECTION ( 'NONE',  ( -1.000000000000000000, -0.000000000000000000, -0.000000000000000000 ) ) ;
#54143=EDGE_CURVE ( 'NONE', #30481, #78412, #30081, .T. ) ;
#54312=ORIENTED_EDGE ( 'NONE', *, *, #37860, .T. ) ;
#54488=EDGE_LOOP ( 'NONE', ( #31517, #62549 ) ) ;
#54565=CARTESIAN_POINT ( 'NONE',  ( 5.550000000000006040, -14.50000000000000178, 11.24599928863593767 ) ) ;
#54609=CARTESIAN_POINT ( 'NONE',  ( 2.000000000000000000, 7.470345474798854293E-16, -6.099999999999999645 ) ) ;
#54764=CARTESIAN_POINT ( 'NONE',  ( 6.983913900142676212, -1.335655600570678558, 18.31352460785937453 ) ) ;
#54911=ORIENTED_EDGE ( 'NONE', *, *, #35247, .F. ) ;
#55000=DIRECTION ( 'NONE',  ( -1.000000000000000000, -0.000000000000000000, -0.000000000000000000 ) ) ;
#55138=VECTOR ( 'NONE', #37050, 1000.000000000000000 ) ;
#55183=CARTESIAN_POINT ( 'NONE',  ( 15.00000000000000533, 0.000000000000000000, 0.000000000000000000 ) ) ;
#55322=DIRECTION ( 'NONE',  ( 0.000000000000000000, -1.000000000000000000, -0.000000000000000000 ) ) ;
#55357=AXIS2_PLACEMENT_3D ( 'NONE', #42175, #80213, #87318 ) ;
#55609=SHAPE_REPRESENTATION ( 'Spool_Varsay\X2\0131\X0\lan', ( #37391 ), #45585 ) ;
#55724=DIRECTION ( 'NONE',  ( 0.000000000000000000, 0.000000000000000000, 1.000000000000000000 ) ) ;
#55736=DIRECTION ( 'NONE',  ( -1.000000000000000000, -0.000000000000000000, -0.000000000000000000 ) ) ;
#55801=CARTESIAN_POINT ( 'NONE',  ( 0.3000000000000007661, 18.50000000000000000, 0.000000000000000000 ) ) ;
#55831=CIRCLE ( 'NONE', #97945, 24.00000000000000000 ) ;
#55866=CIRCLE ( 'NONE', #36428, 19.30000000000000071 ) ;
#56006=AXIS2_PLACEMENT_3D ( 'NONE', #28191, #43917, #63401 ) ;
#56186=AXIS2_PLACEMENT_3D ( 'NONE', #53580, #36344, #36846 ) ;
#56213=ORIENTED_EDGE ( 'NONE', *, *, #52487, .T. ) ;
#56244=EDGE_CURVE ( 'NONE', #63151, #60911, #37516, .T. ) ;
#56373=CARTESIAN_POINT ( 'NONE',  ( 6.150000000000003908, 1.999999999999998224, 19.19609335255483629 ) ) ;
#56482=ORIENTED_EDGE ( 'NONE', *, *, #49730, .F. ) ;
#56713=ORIENTED_EDGE ( 'NONE', *, *, #90659, .T. ) ;
#56727=DIRECTION ( 'NONE',  ( -1.000000000000000000, -0.000000000000000000, -0.000000000000000000 ) ) ;
#56729=VERTEX_POINT ( 'NONE', #22170 ) ;
#56768=ORIENTED_EDGE ( 'NONE', *, *, #94198, .F. ) ;
#56849=CARTESIAN_POINT ( 'NONE',  ( -5.366453405989236813, 0.000000000000000000, 0.000000000000000000 ) ) ;
#56960=ORIENTED_EDGE ( 'NONE', *, *, #53240, .T. ) ;
#56984=LINE ( 'NONE', #87922, #7771 ) ;
#56990=VECTOR ( 'NONE', #70311, 1000.000000000000000 ) ;
#57008=DIRECTION ( 'NONE',  ( 0.000000000000000000, 0.000000000000000000, 1.000000000000000000 ) ) ;
#57032=EDGE_CURVE ( 'NONE', #91284, #94825, #39953, .T. ) ;
#57039=VERTEX_POINT ( 'NONE', #41418 ) ;
#57101=LINE ( 'NONE', #79912, #42112 ) ;
#57153=ADVANCED_FACE ( 'NONE', ( #6339 ), #67760, .T. ) ;
#57175=CARTESIAN_POINT ( 'NONE',  ( 16.00000000000000000, 2.939152317953647894E-15, -24.00000000000000000 ) ) ;
#57233=AXIS2_PLACEMENT_3D ( 'NONE', #97051, #17934, #64641 ) ;
#57554=EDGE_CURVE ( 'NONE', #48655, #30953, #36535, .T. ) ;
#57630=AXIS2_PLACEMENT_3D ( 'NONE', #40314, #71264, #1755 ) ;
#57640=CARTESIAN_POINT ( 'NONE',  ( 7.150000000000004796, -2.000000000000001776, 18.24068255301867936 ) ) ;
#57684=EDGE_LOOP ( 'NONE', ( #88282, #2293, #38575, #33416, #11423, #47053, #78801, #42473, #22079, #5270, #36046, #22288 ) ) ;
#57766=ORIENTED_EDGE ( 'NONE', *, *, #63449, .T. ) ;
#57849=AXIS2_PLACEMENT_3D ( 'NONE', #10477, #26208, #71895 ) ;
#57899=CYLINDRICAL_SURFACE ( 'NONE', #55357, 18.35000000000000142 ) ;
#57912=PLANE ( 'NONE',  #77770 ) ;
#58224=CLOSED_SHELL ( 'NONE', ( #49519, #4471, #50140, #44852, #99296, #38551, #74423, #83, #13353, #77752, #74739, #72241, #65827, #26755, #72121, #58543, #40092, #30333, #53446, #41775, #43347, #82934, #4719, #86714, #64816, #19970, #76694, #27789, #16687, #2504, #51901, #40957, #27435, #90275, #83572, #48315, #9286, #33614, #57153 ) ) ;
#58379=CARTESIAN_POINT ( 'NONE',  ( 9.450000000000002842, -2.000000000000001332, 18.24068255301868291 ) ) ;
#58543=ADVANCED_FACE ( 'NONE', ( #16663 ), #62355, .T. ) ;
#58661=CARTESIAN_POINT ( 'NONE',  ( -5.366453405989237702, 1.999999999999993117, 19.19609335255483984 ) ) ;
#58732=CARTESIAN_POINT ( 'NONE',  ( 6.983857881298739301, -1.335431525194936242, 19.26533332368850182 ) ) ;
#58804=VERTEX_POINT ( 'NONE', #88566 ) ;
#58865=( BOUNDED_CURVE ( )  B_SPLINE_CURVE ( 3, ( #68970, #54764, #17181, #77067 ),
 .UNSPECIFIED., .F., .T. ) 
 B_SPLINE_CURVE_WITH_KNOTS ( ( 4, 4 ),
 ( 4.603180203402792436, 4.712388980384689674 ),
 .UNSPECIFIED. ) 
 CURVE ( )  GEOMETRIC_REPRESENTATION_ITEM ( )  RATIONAL_B_SPLINE_CURVE ( ( 1.000000000000000000, 0.9990063671772055898, 0.9990063671772055898, 1.000000000000000000 ) ) 
 REPRESENTATION_ITEM ( '' )  );
#58956=LINE ( 'NONE', #13752, #77017 ) ;
#58968=EDGE_CURVE ( 'NONE', #60035, #38301, #38099, .T. ) ;
#59013=VECTOR ( 'NONE', #4000, 1000.000000000000000 ) ;
#59106=DIRECTION ( 'NONE',  ( 0.000000000000000000, 0.000000000000000000, 1.000000000000000000 ) ) ;
#59297=CARTESIAN_POINT ( 'NONE',  ( 6.316086099857336045, 1.335655600570672119, 18.31352460785937097 ) ) ;
#59312=ORIENTED_EDGE ( 'NONE', *, *, #49814, .F. ) ;
#59390=AXIS2_PLACEMENT_3D ( 'NONE', #15030, #22631, #98265 ) ;
#59601=CARTESIAN_POINT ( 'NONE',  ( 16.30000000000000071, 0.000000000000000000, 0.000000000000000000 ) ) ;
#59665=VECTOR ( 'NONE', #43898, 1000.000000000000000 ) ;
#59697=EDGE_CURVE ( 'NONE', #46565, #98443, #98240, .T. ) ;
#59718=ORIENTED_EDGE ( 'NONE', *, *, #91676, .F. ) ;
#59807=CARTESIAN_POINT ( 'NONE',  ( 0.6000000000000007550, 0.000000000000000000, 0.000000000000000000 ) ) ;
#59819=ORIENTED_EDGE ( 'NONE', *, *, #16697, .F. ) ;
#59844=AXIS2_PLACEMENT_3D ( 'NONE', #60164, #91086, #21562 ) ;
#59960=DIRECTION ( 'NONE',  ( 0.000000000000000000, 0.000000000000000000, 1.000000000000000000 ) ) ;
#60035=VERTEX_POINT ( 'NONE', #33213 ) ;
#60057=LINE ( 'NONE', #74268, #77751 ) ;
#60085=CARTESIAN_POINT ( 'NONE',  ( 9.616142118701272778, -1.335431525194935798, 19.26533332368850182 ) ) ;
#60125=VECTOR ( 'NONE', #22510, 1000.000000000000000 ) ;
#60164=CARTESIAN_POINT ( 'NONE',  ( 15.00000000000000533, 0.000000000000000000, 0.000000000000000000 ) ) ;
#60205=DIRECTION ( 'NONE',  ( -1.000000000000000000, -0.000000000000000000, -0.000000000000000000 ) ) ;
#60206=CARTESIAN_POINT ( 'NONE',  ( 6.650000000000004796, 0.000000000000000000, 19.30000000000000071 ) ) ;
#60231=ORIENTED_EDGE ( 'NONE', *, *, #38542, .T. ) ;
#60388=DIRECTION ( 'NONE',  ( 1.000000000000000000, 1.387778780781445429E-16, 0.000000000000000000 ) ) ;
#60440=CIRCLE ( 'NONE', #42631, 21.89999999999999858 ) ;
#60471=ORIENTED_EDGE ( 'NONE', *, *, #54143, .T. ) ;
#60611=EDGE_LOOP ( 'NONE', ( #91977, #39945, #20279, #59312 ) ) ;
#60647=DIRECTION ( 'NONE',  ( 1.875376730785737473E-16, -1.000000000000000000, 0.000000000000000000 ) ) ;
#60702=ORIENTED_EDGE ( 'NONE', *, *, #98073, .F. ) ;
#60723=PLANE ( 'NONE',  #5242 ) ;
#60733=FACE_BOUND ( 'NONE', #38954, .T. ) ;
#60851=EDGE_LOOP ( 'NONE', ( #56213, #71129 ) ) ;
#60911=VERTEX_POINT ( 'NONE', #60206 ) ;
#60943=VERTEX_POINT ( 'NONE', #90638 ) ;
#60945=PLANE ( 'NONE',  #16699 ) ;
#60947=ORIENTED_EDGE ( 'NONE', *, *, #38419, .F. ) ;
#61026=AXIS2_PLACEMENT_3D ( 'NONE', #75842, #60647, #28683 ) ;
#61083=ORIENTED_EDGE ( 'NONE', *, *, #89415, .F. ) ;
#61271=( LENGTH_UNIT ( ) NAMED_UNIT ( * ) SI_UNIT ( .MILLI., .METRE. ) );
#61320=EDGE_CURVE ( 'NONE', #11793, #60035, #6406, .T. ) ;
#61346=CARTESIAN_POINT ( 'NONE',  ( -5.366453405989236813, 0.000000000000000000, 0.000000000000000000 ) ) ;
#61431=VECTOR ( 'NONE', #96708, 1000.000000000000000 ) ;
#61566=CARTESIAN_POINT ( 'NONE',  ( -5.366453405989239478, 14.49999999999999645, 11.24599928863594300 ) ) ;
#61707=CARTESIAN_POINT ( 'NONE',  ( -5.366453405989236813, 0.000000000000000000, 24.00000000000000000 ) ) ;
#61937=CARTESIAN_POINT ( 'NONE',  ( 10.45000000000000462, 1.999999999999998668, 24.00000000000000000 ) ) ;
#61958=CARTESIAN_POINT ( 'NONE',  ( 3.300000000000004263, 0.000000000000000000, 0.000000000000000000 ) ) ;
#62272=EDGE_CURVE ( 'NONE', #647, #77342, #9291, .T. ) ;
#62291=DIRECTION ( 'NONE',  ( 0.000000000000000000, 0.000000000000000000, 1.000000000000000000 ) ) ;
#62350=DIRECTION ( 'NONE',  ( 0.000000000000000000, 0.000000000000000000, 1.000000000000000000 ) ) ;
#62355=CYLINDRICAL_SURFACE ( 'NONE', #39867, 24.00000000000000000 ) ;
#62549=ORIENTED_EDGE ( 'NONE', *, *, #76929, .F. ) ;
#62561=ORIENTED_EDGE ( 'NONE', *, *, #61320, .T. ) ;
#62740=EDGE_CURVE ( 'NONE', #76298, #36478, #56984, .T. ) ;
#62813=AXIS2_PLACEMENT_3D ( 'NONE', #56849, #32996, #64474 ) ;
#62855=FACE_OUTER_BOUND ( 'NONE', #7482, .T. ) ;
#62987=CARTESIAN_POINT ( 'NONE',  ( 0.6000000000000007550, 0.000000000000000000, 0.000000000000000000 ) ) ;
#63031=AXIS2_PLACEMENT_3D ( 'NONE', #82172, #28379, #12154 ) ;
#63151=VERTEX_POINT ( 'NONE', #56373 ) ;
#63401=DIRECTION ( 'NONE',  ( 0.000000000000000000, 0.000000000000000000, 1.000000000000000000 ) ) ;
#63447=DIRECTION ( 'NONE',  ( 0.000000000000000000, 0.000000000000000000, 1.000000000000000000 ) ) ;
#63449=EDGE_CURVE ( 'NONE', #78408, #29710, #16761, .T. ) ;
#63475=ORIENTED_EDGE ( 'NONE', *, *, #97033, .F. ) ;
#63591=ORIENTED_EDGE ( 'NONE', *, *, #6192, .T. ) ;
#63617=CIRCLE ( 'NONE', #27957, 21.89999999999999858 ) ;
#63621=PRODUCT_DEFINITION_FORMATION_WITH_SPECIFIED_SOURCE ( 'ANY', '', #27178, .NOT_KNOWN. ) ;
#63647=AXIS2_PLACEMENT_3D ( 'NONE', #62987, #16786, #64504 ) ;
#63770=CARTESIAN_POINT ( 'NONE',  ( 11.05000000000000426, -2.000000000000000888, 19.19609335255483629 ) ) ;
#63812=ORIENTED_EDGE ( 'NONE', *, *, #53240, .F. ) ;
#63888=CARTESIAN_POINT ( 'NONE',  ( 11.05000000000000426, -14.50000000000000178, 11.24599928863593767 ) ) ;
#64180=CARTESIAN_POINT ( 'NONE',  ( 16.00000000000000000, 0.000000000000000000, 24.00000000000000000 ) ) ;
#64331=ORIENTED_EDGE ( 'NONE', *, *, #53424, .T. ) ;
#64443=PLANE ( 'NONE',  #90143 ) ;
#64454=ORIENTED_EDGE ( 'NONE', *, *, #76929, .T. ) ;
#64474=DIRECTION ( 'NONE',  ( 0.000000000000000000, 0.000000000000000000, 1.000000000000000000 ) ) ;
#64483=CARTESIAN_POINT ( 'NONE',  ( 1.600000000000000755, 2.363568322354391830E-15, -19.30000000000000071 ) ) ;
#64504=DIRECTION ( 'NONE',  ( 0.000000000000000000, 0.000000000000000000, 1.000000000000000000 ) ) ;
#64505=ORIENTED_EDGE ( 'NONE', *, *, #7945, .F. ) ;
#64641=DIRECTION ( 'NONE',  ( 0.000000000000000000, 0.000000000000000000, 1.000000000000000000 ) ) ;
#64793=DIRECTION ( 'NONE',  ( 0.000000000000000000, 0.000000000000000000, -1.000000000000000000 ) ) ;
#64816=ADVANCED_FACE ( 'NONE', ( #23808, #79092 ), #39040, .F. ) ;
#64879=CARTESIAN_POINT ( 'NONE',  ( 9.450000000000002842, -2.000000000000001332, 18.24068255301868291 ) ) ;
#64929=ORIENTED_EDGE ( 'NONE', *, *, #22296, .T. ) ;
#65102=CYLINDRICAL_SURFACE ( 'NONE', #28221, 6.099999999999999645 ) ;
#65357=LINE ( 'NONE', #87157, #23943 ) ;
#65375=CARTESIAN_POINT ( 'NONE',  ( 7.150000000000004796, -2.000000000000001776, 19.19609335255483984 ) ) ;
#65469=FACE_OUTER_BOUND ( 'NONE', #42055, .T. ) ;
#65508=EDGE_CURVE ( 'NONE', #68549, #89130, #77340, .T. ) ;
#65567=ORIENTED_EDGE ( 'NONE', *, *, #43964, .F. ) ;
#65654=PLANE ( 'NONE',  #69671 ) ;
#65672=CARTESIAN_POINT ( 'NONE',  ( 3.300000000000004263, 2.247226876435393361E-15, -18.35000000000000142 ) ) ;
#65736=EDGE_LOOP ( 'NONE', ( #34736, #80622, #56960, #60702 ) ) ;
#65827=ADVANCED_FACE ( 'NONE', ( #15321, #22915 ), #6717, .F. ) ;
#65919=CARTESIAN_POINT ( 'NONE',  ( 7.150000000000004796, -2.000000000000001776, 19.19609335255483984 ) ) ;
#66006=DIRECTION ( 'NONE',  ( -1.000000000000000000, -0.000000000000000000, -0.000000000000000000 ) ) ;
#66045=EDGE_LOOP ( 'NONE', ( #25600, #15023 ) ) ;
#66070=VERTEX_POINT ( 'NONE', #41571 ) ;
#66202=EDGE_CURVE ( 'NONE', #21579, #80276, #38436, .T. ) ;
#66302=ORIENTED_EDGE ( 'NONE', *, *, #13972, .T. ) ;
#66316=VERTEX_POINT ( 'NONE', #8492 ) ;
#66394=EDGE_CURVE ( 'NONE', #38489, #21579, #46253, .T. ) ;
#66397=CARTESIAN_POINT ( 'NONE',  ( 1.999999999999998224, 0.000000000000000000, 0.000000000000000000 ) ) ;
#66434=CARTESIAN_POINT ( 'NONE',  ( 6.650000000000004796, 0.000000000000000000, 18.35000000000000142 ) ) ;
#66526=EDGE_CURVE ( 'NONE', #72403, #86308, #88620, .T. ) ;
#66657=DIRECTION ( 'NONE',  ( -0.000000000000000000, 0.000000000000000000, 1.000000000000000000 ) ) ;
#66952=ORIENTED_EDGE ( 'NONE', *, *, #38419, .T. ) ;
#67078=CARTESIAN_POINT ( 'NONE',  ( -5.366453405989236813, 0.000000000000000000, 0.000000000000000000 ) ) ;
#67131=AXIS2_PLACEMENT_3D ( 'NONE', #18459, #41818, #49431 ) ;
#67216=DIRECTION ( 'NONE',  ( 1.000000000000000000, 1.734723475976806848E-16, 0.000000000000000000 ) ) ;
#67226=VERTEX_POINT ( 'NONE', #45807 ) ;
#67268=AXIS2_PLACEMENT_3D ( 'NONE', #30962, #53314, #69029 ) ;
#67346=PLANE ( 'NONE',  #59390 ) ;
#67570=DIRECTION ( 'NONE',  ( -1.000000000000000000, -0.000000000000000000, -0.000000000000000000 ) ) ;
#67637=CARTESIAN_POINT ( 'NONE',  ( -5.366453405989236813, 0.000000000000000000, 18.50000000000000000 ) ) ;
#67646=DIRECTION ( 'NONE',  ( -1.000000000000000000, -0.000000000000000000, -0.000000000000000000 ) ) ;
#67760=PLANE ( 'NONE',  #61026 ) ;
#67840=CARTESIAN_POINT ( 'NONE',  ( -5.366453405989236813, 0.000000000000000000, 0.000000000000000000 ) ) ;
#67897=AXIS2_PLACEMENT_3D ( 'NONE', #41812, #49426, #25566 ) ;
#67946=ORIENTED_EDGE ( 'NONE', *, *, #69992, .F. ) ;
#67948=EDGE_CURVE ( 'NONE', #48682, #68549, #68995, .T. ) ;
#68198=CARTESIAN_POINT ( 'NONE',  ( 11.05000000000000249, 0.000000000000000000, 0.000000000000000000 ) ) ;
#68303=CARTESIAN_POINT ( 'NONE',  ( 1.600000000000000755, 0.000000000000000000, 0.000000000000000000 ) ) ;
#68322=FACE_OUTER_BOUND ( 'NONE', #78365, .T. ) ;
#68362=VERTEX_POINT ( 'NONE', #31304 ) ;
#68448=EDGE_CURVE ( 'NONE', #11793, #29710, #8968, .T. ) ;
#68502=AXIS2_PLACEMENT_3D ( 'NONE', #98276, #36893, #45518 ) ;
#68549=VERTEX_POINT ( 'NONE', #33810 ) ;
#68554=FACE_OUTER_BOUND ( 'NONE', #80919, .T. ) ;
#68593=AXIS2_PLACEMENT_3D ( 'NONE', #66397, #89214, #43045 ) ;
#68626=APPLICATION_CONTEXT ( 'configuration controlled 3d designs of mechanical parts and assemblies' ) ;
#68715=LINE ( 'NONE', #99631, #60125 ) ;
#68783=ORIENTED_EDGE ( 'NONE', *, *, #96068, .F. ) ;
#68921=CIRCLE ( 'NONE', #96447, 18.35000000000000142 ) ;
#68952=CARTESIAN_POINT ( 'NONE',  ( 2.000000000000000000, 0.000000000000000000, 0.000000000000000000 ) ) ;
#68970=CARTESIAN_POINT ( 'NONE',  ( 7.150000000000004796, -2.000000000000001776, 18.24068255301867936 ) ) ;
#68995=CIRCLE ( 'NONE', #91656, 24.00000000000000000 ) ;
#69029=DIRECTION ( 'NONE',  ( 0.000000000000000000, 0.000000000000000000, 1.000000000000000000 ) ) ;
#69038=VECTOR ( 'NONE', #53761, 1000.000000000000000 ) ;
#69671=AXIS2_PLACEMENT_3D ( 'NONE', #35680, #10844, #66657 ) ;
#69690=ORIENTED_EDGE ( 'NONE', *, *, #56244, .T. ) ;
#69831=DIRECTION ( 'NONE',  ( 0.000000000000000000, 0.000000000000000000, 1.000000000000000000 ) ) ;
#69834=EDGE_CURVE ( 'NONE', #60943, #77342, #98208, .T. ) ;
#69912=VERTEX_POINT ( 'NONE', #82003 ) ;
#69990=EDGE_LOOP ( 'NONE', ( #81534, #92870 ) ) ;
#69992=EDGE_CURVE ( 'NONE', #94825, #63151, #51563, .T. ) ;
#70058=DIRECTION ( 'NONE',  ( 0.000000000000000000, 0.000000000000000000, 1.000000000000000000 ) ) ;
#70293=ORIENTED_EDGE ( 'NONE', *, *, #11154, .T. ) ;
#70311=DIRECTION ( 'NONE',  ( -1.000000000000000000, -0.000000000000000000, -0.000000000000000000 ) ) ;
#70323=CARTESIAN_POINT ( 'NONE',  ( 12.92500000000000249, 14.49999999999999645, 12.73734666247253244 ) ) ;
#70541=DIRECTION ( 'NONE',  ( 0.000000000000000000, 0.000000000000000000, -1.000000000000000000 ) ) ;
#70548=EDGE_LOOP ( 'NONE', ( #93726, #97946, #94379, #90382, #40323, #23256, #81753, #60947, #71270, #40661, #50955, #25834 ) ) ;
#70714=CARTESIAN_POINT ( 'NONE',  ( -5.366453405989236813, 7.470345474798854293E-16, -6.099999999999999645 ) ) ;
#71102=DIRECTION ( 'NONE',  ( -1.000000000000000000, 0.000000000000000000, -0.000000000000000000 ) ) ;
#71129=ORIENTED_EDGE ( 'NONE', *, *, #48332, .T. ) ;
#71264=DIRECTION ( 'NONE',  ( -1.000000000000000000, -0.000000000000000000, -0.000000000000000000 ) ) ;
#71270=ORIENTED_EDGE ( 'NONE', *, *, #88021, .F. ) ;
#71362=DIRECTION ( 'NONE',  ( 0.000000000000000000, 0.000000000000000000, 1.000000000000000000 ) ) ;
#71379=DIRECTION ( 'NONE',  ( 0.000000000000000000, 0.000000000000000000, -1.000000000000000000 ) ) ;
#71478=CARTESIAN_POINT ( 'NONE',  ( 15.00000000000000533, 0.000000000000000000, 24.00000000000000000 ) ) ;
#71532=CARTESIAN_POINT ( 'NONE',  ( 3.300000000000004707, 4.450000000000000178, 0.000000000000000000 ) ) ;
#71566=EDGE_CURVE ( 'NONE', #78758, #86308, #7249, .T. ) ;
#71895=DIRECTION ( 'NONE',  ( 0.000000000000000000, 0.000000000000000000, 1.000000000000000000 ) ) ;
#71988=AXIS2_PLACEMENT_3D ( 'NONE', #13327, #67646, #43308 ) ;
#72107=CARTESIAN_POINT ( 'NONE',  ( 5.550000000000004263, -2.000000000000001776, 18.24068255301867936 ) ) ;
#72110=PLANE ( 'NONE',  #38323 ) ;
#72121=ADVANCED_FACE ( 'NONE', ( #26269, #81054 ), #41500, .F. ) ;
#72241=ADVANCED_FACE ( 'NONE', ( #52600 ), #30246, .F. ) ;
#72252=CIRCLE ( 'NONE', #57630, 21.89999999999999858 ) ;
#72347=CARTESIAN_POINT ( 'NONE',  ( -5.366453405989237702, 1.999999999999993117, 18.24068255301867936 ) ) ;
#72403=VERTEX_POINT ( 'NONE', #70323 ) ;
#72512=CARTESIAN_POINT ( 'NONE',  ( 9.950000000000006395, 0.000000000000000000, 18.35000000000000142 ) ) ;
#72549=CARTESIAN_POINT ( 'NONE',  ( 3.675000000000004707, 1.999999999999998224, 24.00000000000000000 ) ) ;
#72604=DIRECTION ( 'NONE',  ( 0.000000000000000000, 0.000000000000000000, -1.000000000000000000 ) ) ;
#72717=FACE_BOUND ( 'NONE', #9127, .T. ) ;
#72882=VECTOR ( 'NONE', #13384, 1000.000000000000000 ) ;
#73216=FACE_OUTER_BOUND ( 'NONE', #52060, .T. ) ;
#73276=EDGE_LOOP ( 'NONE', ( #8077, #5212 ) ) ;
#73367=FACE_OUTER_BOUND ( 'NONE', #18498, .T. ) ;
#73500=CARTESIAN_POINT ( 'NONE',  ( 16.30000000000000071, 2.247226876435393361E-15, -18.35000000000000142 ) ) ;
#73570=FACE_OUTER_BOUND ( 'NONE', #41283, .T. ) ;
#73609=LINE ( 'NONE', #89334, #49136 ) ;
#73622=EDGE_CURVE ( 'NONE', #29598, #12228, #20277, .T. ) ;
#73638=FACE_OUTER_BOUND ( 'NONE', #1521, .T. ) ;
#73669=CARTESIAN_POINT ( 'NONE',  ( 12.92500000000000426, 1.999999999999999556, 19.19609335255483984 ) ) ;
#73768=AXIS2_PLACEMENT_3D ( 'NONE', #7889, #60205, #91624 ) ;
#73807=ORIENTED_EDGE ( 'NONE', *, *, #49730, .T. ) ;
#73818=VERTEX_POINT ( 'NONE', #77925 ) ;
#74142=EDGE_CURVE ( 'NONE', #30481, #48655, #15915, .T. ) ;
#74160=CARTESIAN_POINT ( 'NONE',  ( 0.6000000000000007550, 2.681976490132703452E-15, -21.89999999999999858 ) ) ;
#74208=DIRECTION ( 'NONE',  ( 1.000000000000000000, 0.000000000000000000, 0.000000000000000000 ) ) ;
#74236=FACE_OUTER_BOUND ( 'NONE', #4974, .T. ) ;
#74268=CARTESIAN_POINT ( 'NONE',  ( -5.366453405989236813, 0.000000000000000000, 19.30000000000000071 ) ) ;
#74303=LINE ( 'NONE', #6281, #72882 ) ;
#74418=VECTOR ( 'NONE', #74987, 1000.000000000000000 ) ;
#74423=ADVANCED_FACE ( 'NONE', ( #48889 ), #26033, .F. ) ;
#74677=AXIS2_PLACEMENT_3D ( 'NONE', #7993, #16597, #39948 ) ;
#74691=PLANE ( 'NONE',  #83062 ) ;
#74739=ADVANCED_FACE ( 'NONE', ( #34045 ), #57899, .F. ) ;
#74820=CARTESIAN_POINT ( 'NONE',  ( 10.45000000000000462, 1.999999999999998668, 19.19609335255483984 ) ) ;
#74918=DIRECTION ( 'NONE',  ( -1.000000000000000000, -0.000000000000000000, -0.000000000000000000 ) ) ;
#74986=LINE ( 'NONE', #21200, #59013 ) ;
#74987=DIRECTION ( 'NONE',  ( -1.000000000000000000, -0.000000000000000000, -0.000000000000000000 ) ) ;
#74991=ORIENTED_EDGE ( 'NONE', *, *, #89518, .T. ) ;
#75124=CYLINDRICAL_SURFACE ( 'NONE', #13998, 4.450000000000000178 ) ;
#75144=CIRCLE ( 'NONE', #67131, 21.89999999999999858 ) ;
#75279=CARTESIAN_POINT ( 'NONE',  ( 3.675000000000004707, 0.000000000000000000, 0.000000000000000000 ) ) ;
#75374=CARTESIAN_POINT ( 'NONE',  ( 11.05000000000000604, -14.50000000000000178, 24.00000000000000000 ) ) ;
#75497=DIRECTION ( 'NONE',  ( -1.000000000000000000, -0.000000000000000000, -0.000000000000000000 ) ) ;
#75553=DIRECTION ( 'NONE',  ( -1.000000000000000000, -0.000000000000000000, -0.000000000000000000 ) ) ;
#75745=DIRECTION ( 'NONE',  ( -1.000000000000000000, -0.000000000000000000, -0.000000000000000000 ) ) ;
#75774=CARTESIAN_POINT ( 'NONE',  ( 9.450000000000002842, -2.000000000000001332, 19.19609335255483629 ) ) ;
#75842=CARTESIAN_POINT ( 'NONE',  ( 12.92500000000000249, 14.50000000000000000, 24.00000000000000000 ) ) ;
#76089=DIRECTION ( 'NONE',  ( 1.000000000000000000, 0.000000000000000000, 0.000000000000000000 ) ) ;
#76093=ORIENTED_EDGE ( 'NONE', *, *, #41439, .T. ) ;
#76216=DIRECTION ( 'NONE',  ( -1.000000000000000000, -0.000000000000000000, -0.000000000000000000 ) ) ;
#76266=ORIENTED_EDGE ( 'NONE', *, *, #2594, .T. ) ;
#76270=DIRECTION ( 'NONE',  ( -1.000000000000000000, -1.734723475976806848E-16, -0.000000000000000000 ) ) ;
#76298=VERTEX_POINT ( 'NONE', #17032 ) ;
#76409=DIRECTION ( 'NONE',  ( -0.000000000000000000, 1.000000000000000000, 0.000000000000000000 ) ) ;
#76434=CARTESIAN_POINT ( 'NONE',  ( 3.675000000000004707, 1.999999999999998224, 18.24068255301867936 ) ) ;
#76460=CARTESIAN_POINT ( 'NONE',  ( 3.675000000000004707, 1.999999999999998224, 24.00000000000000000 ) ) ;
#76483=ORIENTED_EDGE ( 'NONE', *, *, #94242, .T. ) ;
#76533=DIRECTION ( 'NONE',  ( 0.000000000000000000, 0.000000000000000000, 1.000000000000000000 ) ) ;
#76549=LINE ( 'NONE', #44628, #94386 ) ;
#76624=CIRCLE ( 'NONE', #24781, 19.30000000000000071 ) ;
#76690=AXIS2_PLACEMENT_3D ( 'NONE', #85159, #55736, #100362 ) ;
#76694=ADVANCED_FACE ( 'NONE', ( #72717, #73216 ), #74691, .F. ) ;
#76706=LINE ( 'NONE', #67637, #88444 ) ;
#76901=EDGE_CURVE ( 'NONE', #20703, #91990, #23386, .T. ) ;
#76929=EDGE_CURVE ( 'NONE', #24851, #1763, #63617, .T. ) ;
#77004=VECTOR ( 'NONE', #53173, 1000.000000000000000 ) ;
#77017=VECTOR ( 'NONE', #83769, 1000.000000000000000 ) ;
#77067=CARTESIAN_POINT ( 'NONE',  ( 6.650000000000004796, 0.000000000000000000, 18.35000000000000142 ) ) ;
#77097=LINE ( 'NONE', #78588, #79391 ) ;
#77140=DIRECTION ( 'NONE',  ( -0.9701425001453318764, 0.2425356250363331356, 0.000000000000000000 ) ) ;
#77340=LINE ( 'NONE', #100164, #53273 ) ;
#77342=VERTEX_POINT ( 'NONE', #63888 ) ;
#77405=PLANE ( 'NONE',  #49914 ) ;
#77435=CARTESIAN_POINT ( 'NONE',  ( -5.366453405989235925, -2.000000000000005329, 19.19609335255483629 ) ) ;
#77538=CARTESIAN_POINT ( 'NONE',  ( 15.00000000000000533, 0.000000000000000000, 19.30000000000000071 ) ) ;
#77546=DIRECTION ( 'NONE',  ( -1.000000000000000000, -0.000000000000000000, -0.000000000000000000 ) ) ;
#77677=CARTESIAN_POINT ( 'NONE',  ( -5.366453405989236813, 0.000000000000000000, 21.89999999999999858 ) ) ;
#77751=VECTOR ( 'NONE', #5749, 1000.000000000000000 ) ;
#77752=ADVANCED_FACE ( 'NONE', ( #30786 ), #92673, .T. ) ;
#77770=AXIS2_PLACEMENT_3D ( 'NONE', #88856, #19321, #50292 ) ;
#77925=CARTESIAN_POINT ( 'NONE',  ( 15.00000000000000533, 2.939152317953647894E-15, -24.00000000000000000 ) ) ;
#78041=DIRECTION ( 'NONE',  ( -1.000000000000000000, -0.000000000000000000, -0.000000000000000000 ) ) ;
#78111=ORIENTED_EDGE ( 'NONE', *, *, #69834, .T. ) ;
#78123=ORIENTED_EDGE ( 'NONE', *, *, #9698, .F. ) ;
#78139=EDGE_CURVE ( 'NONE', #76298, #60943, #73609, .T. ) ;
#78365=EDGE_LOOP ( 'NONE', ( #10775, #98110, #17518, #9231 ) ) ;
#78393=EDGE_CURVE ( 'NONE', #21579, #38489, #84805, .T. ) ;
#78408=VERTEX_POINT ( 'NONE', #26812 ) ;
#78412=VERTEX_POINT ( 'NONE', #96818 ) ;
#78526=EDGE_CURVE ( 'NONE', #2943, #66070, #24837, .T. ) ;
#78535=CYLINDRICAL_SURFACE ( 'NONE', #94533, 21.89999999999999858 ) ;
#78550=DIRECTION ( 'NONE',  ( -1.000000000000000000, -0.000000000000000000, -0.000000000000000000 ) ) ;
#78573=EDGE_CURVE ( 'NONE', #66070, #56729, #89713, .T. ) ;
#78576=DIRECTION ( 'NONE',  ( -1.000000000000000000, -0.000000000000000000, -0.000000000000000000 ) ) ;
#78588=CARTESIAN_POINT ( 'NONE',  ( 3.675000000000002487, 14.49999999999999822, 24.00000000000000000 ) ) ;
#78596=DIRECTION ( 'NONE',  ( 1.000000000000000000, 0.000000000000000000, 0.000000000000000000 ) ) ;
#78610=FACE_OUTER_BOUND ( 'NONE', #66045, .T. ) ;
#78613=ORIENTED_EDGE ( 'NONE', *, *, #12988, .F. ) ;
#78755=ORIENTED_EDGE ( 'NONE', *, *, #68448, .T. ) ;
#78758=VERTEX_POINT ( 'NONE', #98298 ) ;
#78801=ORIENTED_EDGE ( 'NONE', *, *, #13972, .F. ) ;
#78919=ORIENTED_EDGE ( 'NONE', *, *, #32947, .F. ) ;
#78972=CARTESIAN_POINT ( 'NONE',  ( 9.450000000000002842, -2.000000000000001332, 24.00000000000000000 ) ) ;
#78993=( BOUNDED_CURVE ( )  B_SPLINE_CURVE ( 3, ( #26284, #89680, #58732, #65375 ),
 .UNSPECIFIED., .F., .F. ) 
 B_SPLINE_CURVE_WITH_KNOTS ( ( 4, 4 ),
 ( 1.570796326794896558, 1.674609638881183304 ),
 .UNSPECIFIED. ) 
 CURVE ( )  GEOMETRIC_REPRESENTATION_ITEM ( )  RATIONAL_B_SPLINE_CURVE ( ( 1.000000000000000000, 0.9991021013140741758, 0.9991021013140741758, 1.000000000000000000 ) ) 
 REPRESENTATION_ITEM ( '' )  );
#79092=FACE_OUTER_BOUND ( 'NONE', #95604, .T. ) ;
#79391=VECTOR ( 'NONE', #85220, 1000.000000000000000 ) ;
#79414=ORIENTED_EDGE ( 'NONE', *, *, #7945, .T. ) ;
#79551=CARTESIAN_POINT ( 'NONE',  ( 0.6000000000000009770, 21.89999999999999858, 0.000000000000000000 ) ) ;
#79626=DIRECTION ( 'NONE',  ( -0.000000000000000000, 0.000000000000000000, 1.000000000000000000 ) ) ;
#79665=CARTESIAN_POINT ( 'NONE',  ( 10.45000000000000462, 1.999999999999998668, 19.19609335255483984 ) ) ;
#79843=CIRCLE ( 'NONE', #63647, 24.00000000000000000 ) ;
#79912=CARTESIAN_POINT ( 'NONE',  ( -5.366453405989236813, 2.939152317953647894E-15, -24.00000000000000000 ) ) ;
#80047=DIRECTION ( 'NONE',  ( 0.000000000000000000, 0.000000000000000000, -1.000000000000000000 ) ) ;
#80166=ORIENTED_EDGE ( 'NONE', *, *, #58968, .F. ) ;
#80213=DIRECTION ( 'NONE',  ( -1.000000000000000000, -0.000000000000000000, -0.000000000000000000 ) ) ;
#80223=AXIS2_PLACEMENT_3D ( 'NONE', #2037, #55322, #8635 ) ;
#80276=VERTEX_POINT ( 'NONE', #64483 ) ;
#80330=DIRECTION ( 'NONE',  ( 0.000000000000000000, 0.000000000000000000, 1.000000000000000000 ) ) ;
#80622=ORIENTED_EDGE ( 'NONE', *, *, #7319, .T. ) ;
#80666=ORIENTED_EDGE ( 'NONE', *, *, #57032, .F. ) ;
#80919=EDGE_LOOP ( 'NONE', ( #61083, #38461, #25633, #59718 ) ) ;
#80976=ORIENTED_EDGE ( 'NONE', *, *, #51042, .T. ) ;
#81054=FACE_OUTER_BOUND ( 'NONE', #51565, .T. ) ;
#81152=LINE ( 'NONE', #72549, #99811 ) ;
#81390=CARTESIAN_POINT ( 'NONE',  ( 15.00000000000000533, 2.363568322354391830E-15, -19.30000000000000071 ) ) ;
#81514=AXIS2_PLACEMENT_3D ( 'NONE', #86530, #95651, #17016 ) ;
#81534=ORIENTED_EDGE ( 'NONE', *, *, #52710, .T. ) ;
#81600=CARTESIAN_POINT ( 'NONE',  ( -5.366453405989236813, 2.265596578422603396E-15, -18.50000000000000000 ) ) ;
#81620=CARTESIAN_POINT ( 'NONE',  ( 11.05000000000000426, -2.000000000000000888, 24.00000000000000000 ) ) ;
#81753=ORIENTED_EDGE ( 'NONE', *, *, #78139, .F. ) ;
#81984=EDGE_CURVE ( 'NONE', #30953, #48655, #19496, .T. ) ;
#81996=EDGE_CURVE ( 'NONE', #60911, #49715, #78993, .T. ) ;
#82003=CARTESIAN_POINT ( 'NONE',  ( 12.92500000000000426, 1.999999999999999556, 18.24068255301867936 ) ) ;
#82172=CARTESIAN_POINT ( 'NONE',  ( 11.05000000000000426, -2.000000000000000888, 24.00000000000000000 ) ) ;
#82222=LINE ( 'NONE', #44172, #55138 ) ;
#82252=( BOUNDED_CURVE ( )  B_SPLINE_CURVE ( 3, ( #17716, #48685, #11098, #72512 ),
 .UNSPECIFIED., .F., .F. ) 
 B_SPLINE_CURVE_WITH_KNOTS ( ( 4, 4 ),
 ( 4.603180203402792436, 4.712388980384689674 ),
 .UNSPECIFIED. ) 
 CURVE ( )  GEOMETRIC_REPRESENTATION_ITEM ( )  RATIONAL_B_SPLINE_CURVE ( ( 1.000000000000000000, 0.9990063671772055898, 0.9990063671772055898, 1.000000000000000000 ) ) 
 REPRESENTATION_ITEM ( '' )  );
#82253=ORIENTED_EDGE ( 'NONE', *, *, #71566, .F. ) ;
#82469=CYLINDRICAL_SURFACE ( 'NONE', #56006, 19.30000000000000071 ) ;
#82492=DIRECTION ( 'NONE',  ( 1.000000000000000000, 0.000000000000000000, 0.000000000000000000 ) ) ;
#82545=EDGE_CURVE ( 'NONE', #69912, #85731, #41906, .T. ) ;
#82764=CARTESIAN_POINT ( 'NONE',  ( 3.300000000000006040, 0.000000000000000000, 0.000000000000000000 ) ) ;
#82934=ADVANCED_FACE ( 'NONE', ( #40654, #9186 ), #72110, .F. ) ;
#83014=CIRCLE ( 'NONE', #87955, 18.35000000000000142 ) ;
#83062=AXIS2_PLACEMENT_3D ( 'NONE', #10807, #74208, #5186 ) ;
#83188=PLANE ( 'NONE',  #10224 ) ;
#83273=ORIENTED_EDGE ( 'NONE', *, *, #48332, .F. ) ;
#83505=VECTOR ( 'NONE', #19312, 1000.000000000000000 ) ;
#83572=ADVANCED_FACE ( 'NONE', ( #50239 ), #3071, .T. ) ;
#83701=CARTESIAN_POINT ( 'NONE',  ( 6.482958569640026703, 0.6681657214399144840, 19.30000000000000071 ) ) ;
#83761=FACE_OUTER_BOUND ( 'NONE', #93589, .T. ) ;
#83769=DIRECTION ( 'NONE',  ( -1.000000000000000000, -0.000000000000000000, -0.000000000000000000 ) ) ;
#84131=AXIS2_PLACEMENT_3D ( 'NONE', #44008, #36895, #99765 ) ;
#84144=ORIENTED_EDGE ( 'NONE', *, *, #65508, .F. ) ;
#84208=DIRECTION ( 'NONE',  ( 0.000000000000000000, 0.000000000000000000, 1.000000000000000000 ) ) ;
#84248=EDGE_CURVE ( 'NONE', #91990, #47093, #45008, .T. ) ;
#84331=DIRECTION ( 'NONE',  ( -1.418030089354338178E-16, 1.000000000000000000, 0.000000000000000000 ) ) ;
#84536=ORIENTED_EDGE ( 'NONE', *, *, #39641, .T. ) ;
#84748=EDGE_LOOP ( 'NONE', ( #33642, #90258, #84536, #44679 ) ) ;
#84805=CIRCLE ( 'NONE', #44336, 19.30000000000000071 ) ;
#85001=DIRECTION ( 'NONE',  ( -1.000000000000000000, -0.000000000000000000, -0.000000000000000000 ) ) ;
#85081=ORIENTED_EDGE ( 'NONE', *, *, #9698, .T. ) ;
#85103=CARTESIAN_POINT ( 'NONE',  ( -5.366453405989236813, 0.000000000000000000, 21.89999999999999858 ) ) ;
#85141=AXIS2_PLACEMENT_3D ( 'NONE', #68303, #45970, #92127 ) ;
#85159=CARTESIAN_POINT ( 'NONE',  ( 3.300000000000004263, 0.000000000000000000, 0.000000000000000000 ) ) ;
#85220=DIRECTION ( 'NONE',  ( 0.000000000000000000, 0.000000000000000000, -1.000000000000000000 ) ) ;
#85309=MECHANICAL_CONTEXT ( 'NONE', #49246, 'mechanical' ) ;
#85373=ORIENTED_EDGE ( 'NONE', *, *, #76901, .F. ) ;
#85444=FACE_OUTER_BOUND ( 'NONE', #9044, .T. ) ;
#85702=VECTOR ( 'NONE', #85001, 1000.000000000000000 ) ;
#85731=VERTEX_POINT ( 'NONE', #53012 ) ;
#85871=ORIENTED_EDGE ( 'NONE', *, *, #43964, .T. ) ;
#85970=ORIENTED_EDGE ( 'NONE', *, *, #78573, .T. ) ;
#86077=DIRECTION ( 'NONE',  ( -1.000000000000000000, -0.000000000000000000, -0.000000000000000000 ) ) ;
#86084=( NAMED_UNIT ( * ) PLANE_ANGLE_UNIT ( ) SI_UNIT ( $, .RADIAN. ) );
#86224=DIRECTION ( 'NONE',  ( 0.000000000000000000, 0.000000000000000000, 1.000000000000000000 ) ) ;
#86308=VERTEX_POINT ( 'NONE', #14795 ) ;
#86352=CIRCLE ( 'NONE', #81514, 21.89999999999999858 ) ;
#86530=CARTESIAN_POINT ( 'NONE',  ( 0.3000000000000007661, 0.000000000000000000, 0.000000000000000000 ) ) ;
#86633=EDGE_LOOP ( 'NONE', ( #65567, #22799 ) ) ;
#86667=CIRCLE ( 'NONE', #46249, 4.450000000000000178 ) ;
#86714=ADVANCED_FACE ( 'NONE', ( #100275 ), #93685, .F. ) ;
#86735=AXIS2_PLACEMENT_3D ( 'NONE', #92620, #54089, #29735 ) ;
#86967=ORIENTED_EDGE ( 'NONE', *, *, #97462, .T. ) ;
#87048=CARTESIAN_POINT ( 'NONE',  ( 16.30000000000000071, 0.000000000000000000, 0.000000000000000000 ) ) ;
#87157=CARTESIAN_POINT ( 'NONE',  ( -5.366453405989239478, 14.49999999999999645, 12.73734666247253244 ) ) ;
#87318=DIRECTION ( 'NONE',  ( 0.000000000000000000, 0.000000000000000000, 1.000000000000000000 ) ) ;
#87712=CIRCLE ( 'NONE', #98983, 21.89999999999999858 ) ;
#87904=PRODUCT_DEFINITION_SHAPE ( 'NONE', 'NONE',  #19046 ) ;
#87922=CARTESIAN_POINT ( 'NONE',  ( 5.550000000000006040, -14.50000000000000178, 24.00000000000000000 ) ) ;
#87955=AXIS2_PLACEMENT_3D ( 'NONE', #25757, #56727, #55724 ) ;
#88021=EDGE_CURVE ( 'NONE', #49715, #15581, #9378, .T. ) ;
#88038=DIRECTION ( 'NONE',  ( -1.000000000000000000, -0.000000000000000000, -0.000000000000000000 ) ) ;
#88135=CIRCLE ( 'NONE', #5542, 19.30000000000000071 ) ;
#88282=ORIENTED_EDGE ( 'NONE', *, *, #37326, .F. ) ;
#88444=VECTOR ( 'NONE', #76216, 1000.000000000000000 ) ;
#88566=CARTESIAN_POINT ( 'NONE',  ( 3.300000000000004263, 0.000000000000000000, 18.35000000000000142 ) ) ;
#88620=LINE ( 'NONE', #11985, #30015 ) ;
#88675=DIRECTION ( 'NONE',  ( 1.000000000000000000, 0.000000000000000000, 0.000000000000000000 ) ) ;
#88739=CARTESIAN_POINT ( 'NONE',  ( 11.05000000000000249, 0.000000000000000000, 0.000000000000000000 ) ) ;
#88847=CARTESIAN_POINT ( 'NONE',  ( -5.366453405989236813, 0.000000000000000000, 4.450000000000000178 ) ) ;
#88856=CARTESIAN_POINT ( 'NONE',  ( 6.150000000000003908, 1.999999999999998224, 24.00000000000000000 ) ) ;
#88953=AXIS2_PLACEMENT_3D ( 'NONE', #96592, #88993, #25585 ) ;
#88993=DIRECTION ( 'NONE',  ( -1.000000000000000000, -0.000000000000000000, -0.000000000000000000 ) ) ;
#89092=EDGE_LOOP ( 'NONE', ( #90845, #96088 ) ) ;
#89130=VERTEX_POINT ( 'NONE', #97865 ) ;
#89214=DIRECTION ( 'NONE',  ( -1.000000000000000000, -0.000000000000000000, -0.000000000000000000 ) ) ;
#89334=CARTESIAN_POINT ( 'NONE',  ( -5.366453405989236813, -14.50000000000000178, 12.73734666247252711 ) ) ;
#89415=EDGE_CURVE ( 'NONE', #98443, #73818, #57101, .T. ) ;
#89518=EDGE_CURVE ( 'NONE', #67226, #47093, #74303, .T. ) ;
#89535=VECTOR ( 'NONE', #8189, 1000.000000000000000 ) ;
#89609=DIRECTION ( 'NONE',  ( 1.000000000000000000, 0.000000000000000000, 0.000000000000000000 ) ) ;
#89680=CARTESIAN_POINT ( 'NONE',  ( 6.817041430359983778, -0.6681657214399134848, 19.30000000000000071 ) ) ;
#89713=LINE ( 'NONE', #81600, #36218 ) ;
#89740=VERTEX_POINT ( 'NONE', #663 ) ;
#89857=DIRECTION ( 'NONE',  ( 0.000000000000000000, 0.000000000000000000, 1.000000000000000000 ) ) ;
#90135=ORIENTED_EDGE ( 'NONE', *, *, #74142, .T. ) ;
#90143=AXIS2_PLACEMENT_3D ( 'NONE', #71532, #26348, #79626 ) ;
#90258=ORIENTED_EDGE ( 'NONE', *, *, #16697, .T. ) ;
#90275=ADVANCED_FACE ( 'NONE', ( #73570 ), #13644, .T. ) ;
#90382=ORIENTED_EDGE ( 'NONE', *, *, #61320, .F. ) ;
#90547=ORIENTED_EDGE ( 'NONE', *, *, #27228, .F. ) ;
#90597=LINE ( 'NONE', #44436, #61431 ) ;
#90638=CARTESIAN_POINT ( 'NONE',  ( 11.05000000000000426, -14.50000000000000178, 12.73734666247252711 ) ) ;
#90659=EDGE_CURVE ( 'NONE', #78412, #30481, #90761, .T. ) ;
#90761=CIRCLE ( 'NONE', #88953, 6.099999999999999645 ) ;
#90845=ORIENTED_EDGE ( 'NONE', *, *, #67948, .F. ) ;
#91086=DIRECTION ( 'NONE',  ( -1.000000000000000000, -0.000000000000000000, -0.000000000000000000 ) ) ;
#91225=ORIENTED_EDGE ( 'NONE', *, *, #66202, .T. ) ;
#91284=VERTEX_POINT ( 'NONE', #39505 ) ;
#91311=DIRECTION ( 'NONE',  ( -1.387778780781445429E-16, 1.000000000000000000, 0.000000000000000000 ) ) ;
#91567=VECTOR ( 'NONE', #53636, 1000.000000000000000 ) ;
#91624=DIRECTION ( 'NONE',  ( 0.000000000000000000, 0.000000000000000000, 1.000000000000000000 ) ) ;
#91652=CARTESIAN_POINT ( 'NONE',  ( 16.00000000000000000, 0.000000000000000000, 0.000000000000000000 ) ) ;
#91656=AXIS2_PLACEMENT_3D ( 'NONE', #7591, #15202, #84208 ) ;
#91676=EDGE_CURVE ( 'NONE', #73818, #42982, #92197, .T. ) ;
#91714=AXIS2_PLACEMENT_3D ( 'NONE', #61958, #23363, #70058 ) ;
#91754=ORIENTED_EDGE ( 'NONE', *, *, #98073, .T. ) ;
#91806=CARTESIAN_POINT ( 'NONE',  ( 5.550000000000004263, -2.000000000000001776, 24.00000000000000000 ) ) ;
#91934=AXIS2_PLACEMENT_3D ( 'NONE', #68198, #43377, #99128 ) ;
#91977=ORIENTED_EDGE ( 'NONE', *, *, #89518, .F. ) ;
#91990=VERTEX_POINT ( 'NONE', #30054 ) ;
#92127=DIRECTION ( 'NONE',  ( 0.000000000000000000, 0.000000000000000000, 1.000000000000000000 ) ) ;
#92164=FACE_OUTER_BOUND ( 'NONE', #89092, .T. ) ;
#92191=SHAPE_REPRESENTATION_RELATIONSHIP ( 'NONE' , 'NONE' ,  #55609, #29431 ) ;
#92197=CIRCLE ( 'NONE', #59844, 24.00000000000000000 ) ;
#92470=CARTESIAN_POINT ( 'NONE',  ( -5.366453405989236813, 2.247226876435393361E-15, -18.35000000000000142 ) ) ;
#92490=DIRECTION ( 'NONE',  ( 1.000000000000000000, 0.000000000000000000, 0.000000000000000000 ) ) ;
#92618=ORIENTED_EDGE ( 'NONE', *, *, #66394, .F. ) ;
#92620=CARTESIAN_POINT ( 'NONE',  ( 1.600000000000000755, 0.000000000000000000, 0.000000000000000000 ) ) ;
#92673=CYLINDRICAL_SURFACE ( 'NONE', #28035, 19.30000000000000071 ) ;
#92870=ORIENTED_EDGE ( 'NONE', *, *, #91676, .T. ) ;
#93483=AXIS2_PLACEMENT_3D ( 'NONE', #12400, #67216, #34754 ) ;
#93510=DIRECTION ( 'NONE',  ( -1.000000000000000000, -0.000000000000000000, -0.000000000000000000 ) ) ;
#93589=EDGE_LOOP ( 'NONE', ( #62561, #24864, #64929, #49498, #57766, #51692 ) ) ;
#93659=DIRECTION ( 'NONE',  ( -0.000000000000000000, 0.000000000000000000, 1.000000000000000000 ) ) ;
#93685=CYLINDRICAL_SURFACE ( 'NONE', #93728, 4.450000000000000178 ) ;
#93726=ORIENTED_EDGE ( 'NONE', *, *, #66202, .F. ) ;
#93728=AXIS2_PLACEMENT_3D ( 'NONE', #38905, #86077, #30796 ) ;
#93829=ORIENTED_EDGE ( 'NONE', *, *, #52665, .F. ) ;
#94198=EDGE_CURVE ( 'NONE', #37020, #69912, #23791, .T. ) ;
#94242=EDGE_CURVE ( 'NONE', #12228, #7941, #58865, .T. ) ;
#94280=DIRECTION ( 'NONE',  ( 0.000000000000000000, 0.000000000000000000, 1.000000000000000000 ) ) ;
#94379=ORIENTED_EDGE ( 'NONE', *, *, #35008, .T. ) ;
#94386=VECTOR ( 'NONE', #75553, 1000.000000000000000 ) ;
#94533=AXIS2_PLACEMENT_3D ( 'NONE', #61346, #46112, #76533 ) ;
#94543=DIRECTION ( 'NONE',  ( -1.000000000000000000, -0.000000000000000000, -0.000000000000000000 ) ) ;
#94825=VERTEX_POINT ( 'NONE', #33280 ) ;
#94980=ORIENTED_EDGE ( 'NONE', *, *, #5097, .T. ) ;
#95604=EDGE_LOOP ( 'NONE', ( #7287, #14107 ) ) ;
#95651=DIRECTION ( 'NONE',  ( -1.000000000000000000, -0.000000000000000000, -0.000000000000000000 ) ) ;
#95791=DIRECTION ( 'NONE',  ( -1.000000000000000000, -0.000000000000000000, -0.000000000000000000 ) ) ;
#95802=LINE ( 'NONE', #3968, #3995 ) ;
#96021=CARTESIAN_POINT ( 'NONE',  ( -5.366453405989236813, 0.000000000000000000, 0.000000000000000000 ) ) ;
#96068=EDGE_CURVE ( 'NONE', #98443, #46565, #11174, .T. ) ;
#96088=ORIENTED_EDGE ( 'NONE', *, *, #51851, .F. ) ;
#96126=EDGE_LOOP ( 'NONE', ( #85081, #74991, #22446, #85373 ) ) ;
#96342=DIRECTION ( 'NONE',  ( 1.797640907747986603E-16, -1.000000000000000000, 0.000000000000000000 ) ) ;
#96447=AXIS2_PLACEMENT_3D ( 'NONE', #75279, #76270, #5772 ) ;
#96453=FACE_OUTER_BOUND ( 'NONE', #31295, .T. ) ;
#96548=ORIENTED_EDGE ( 'NONE', *, *, #15080, .T. ) ;
#96580=VECTOR ( 'NONE', #64793, 1000.000000000000000 ) ;
#96592=CARTESIAN_POINT ( 'NONE',  ( 2.000000000000000000, 0.000000000000000000, 0.000000000000000000 ) ) ;
#96638=CARTESIAN_POINT ( 'NONE',  ( 0.6000000000000007550, 0.000000000000000000, 0.000000000000000000 ) ) ;
#96708=DIRECTION ( 'NONE',  ( -1.000000000000000000, -0.000000000000000000, -0.000000000000000000 ) ) ;
#96719=DIRECTION ( 'NONE',  ( 0.000000000000000000, 0.000000000000000000, -1.000000000000000000 ) ) ;
#96791=CARTESIAN_POINT ( 'NONE',  ( 0.000000000000000000, 0.000000000000000000, 0.000000000000000000 ) ) ;
#96818=CARTESIAN_POINT ( 'NONE',  ( 2.000000000000000000, 0.000000000000000000, 6.099999999999999645 ) ) ;
#96851=ORIENTED_EDGE ( 'NONE', *, *, #54041, .T. ) ;
#96888=CYLINDRICAL_SURFACE ( 'NONE', #62813, 21.89999999999999858 ) ;
#97018=DIRECTION ( 'NONE',  ( 0.000000000000000000, 0.000000000000000000, 1.000000000000000000 ) ) ;
#97033=EDGE_CURVE ( 'NONE', #41466, #647, #50674, .T. ) ;
#97051=CARTESIAN_POINT ( 'NONE',  ( 0.000000000000000000, 0.000000000000000000, 0.000000000000000000 ) ) ;
#97286=VECTOR ( 'NONE', #92490, 1000.000000000000000 ) ;
#97462=EDGE_CURVE ( 'NONE', #49715, #12228, #18309, .T. ) ;
#97773=CARTESIAN_POINT ( 'NONE',  ( 0.3000000000000007661, 2.681976490132703452E-15, -21.89999999999999858 ) ) ;
#97865=CARTESIAN_POINT ( 'NONE',  ( 0.6000000000000007550, 2.939152317953647894E-15, -24.00000000000000000 ) ) ;
#97898=ORIENTED_EDGE ( 'NONE', *, *, #66394, .T. ) ;
#97945=AXIS2_PLACEMENT_3D ( 'NONE', #59807, #75497, #21214 ) ;
#97946=ORIENTED_EDGE ( 'NONE', *, *, #78393, .T. ) ;
#98073=EDGE_CURVE ( 'NONE', #91284, #78758, #77097, .T. ) ;
#98110=ORIENTED_EDGE ( 'NONE', *, *, #94198, .T. ) ;
#98208=LINE ( 'NONE', #75374, #22586 ) ;
#98232=CIRCLE ( 'NONE', #33413, 18.50000000000000000 ) ;
#98240=CIRCLE ( 'NONE', #7565, 24.00000000000000000 ) ;
#98265=DIRECTION ( 'NONE',  ( 0.000000000000000000, 0.000000000000000000, -1.000000000000000000 ) ) ;
#98276=CARTESIAN_POINT ( 'NONE',  ( -5.366453405989236813, 0.000000000000000000, 0.000000000000000000 ) ) ;
#98298=CARTESIAN_POINT ( 'NONE',  ( 3.675000000000002043, 14.49999999999999645, 11.24599928863594300 ) ) ;
#98305=EDGE_LOOP ( 'NONE', ( #19576, #60471, #76266, #22844 ) ) ;
#98321=DIRECTION ( 'NONE',  ( -1.000000000000000000, -1.387778780781445429E-16, -0.000000000000000000 ) ) ;
#98443=VERTEX_POINT ( 'NONE', #57175 ) ;
#98884=DIRECTION ( 'NONE',  ( 1.000000000000000000, 1.387778780781445429E-16, 0.000000000000000000 ) ) ;
#98983=AXIS2_PLACEMENT_3D ( 'NONE', #87048, #25141, #69831 ) ;
#99122=ORIENTED_EDGE ( 'NONE', *, *, #66526, .T. ) ;
#99128=DIRECTION ( 'NONE',  ( 9.453533929028921186E-17, -1.000000000000000000, -8.881784197001252323E-16 ) ) ;
#99296=ADVANCED_FACE ( 'NONE', ( #46071 ), #8994, .T. ) ;
#99305=AXIS2_PLACEMENT_3D ( 'NONE', #38399, #840, #71362 ) ;
#99422=CARTESIAN_POINT ( 'NONE',  ( 6.316142118701270292, 1.335431525194935798, 19.26533332368850182 ) ) ;
#99631=CARTESIAN_POINT ( 'NONE',  ( -5.366453405989236813, -14.50000000000000178, 11.24599928863593767 ) ) ;
#99736=CARTESIAN_POINT ( 'NONE',  ( 5.550000000000006040, -14.50000000000000178, 24.00000000000000000 ) ) ;
#99765=DIRECTION ( 'NONE',  ( 0.000000000000000000, 0.000000000000000000, 1.000000000000000000 ) ) ;
#99811=VECTOR ( 'NONE', #3041, 1000.000000000000000 ) ;
#99950=EDGE_LOOP ( 'NONE', ( #54911, #17019, #6251, #41724, #12793, #78919, #82253, #63812, #14070, #5867, #43327, #60231 ) ) ;
#100125=DIRECTION ( 'NONE',  ( 0.000000000000000000, 0.000000000000000000, 1.000000000000000000 ) ) ;
#100164=CARTESIAN_POINT ( 'NONE',  ( -5.366453405989236813, 2.939152317953647894E-15, -24.00000000000000000 ) ) ;
#100242=DIRECTION ( 'NONE',  ( 0.000000000000000000, 0.000000000000000000, 1.000000000000000000 ) ) ;
#100275=FACE_OUTER_BOUND ( 'NONE', #52497, .T. ) ;
#100311=( BOUNDED_CURVE ( )  B_SPLINE_CURVE ( 3, ( #66434, #18722, #59297, #28337 ),
 .UNSPECIFIED., .F., .T. ) 
 B_SPLINE_CURVE_WITH_KNOTS ( ( 4, 4 ),
 ( 4.712388980384689674, 4.821597757366586912 ),
 .UNSPECIFIED. ) 
 CURVE ( )  GEOMETRIC_REPRESENTATION_ITEM ( )  RATIONAL_B_SPLINE_CURVE ( ( 1.000000000000000000, 0.9990063671772055898, 0.9990063671772055898, 1.000000000000000000 ) ) 
 REPRESENTATION_ITEM ( '' )  );
#100362=DIRECTION ( 'NONE',  ( 0.000000000000000000, 0.000000000000000000, 1.000000000000000000 ) ) ;
#100441=COLOUR_RGB('Light Blue', 0.31764706, 0.68627451, 0.89019608);
#100442=FILL_AREA_STYLE_COLOUR('',#100441);
#100443=FILL_AREA_STYLE('',(#100442));
#100444=SURFACE_STYLE_FILL_AREA(#100443);
#100445=SURFACE_SIDE_STYLE('',(#100444));
#100446=SURFACE_STYLE_USAGE(.BOTH.,#100445);
#100447=PRESENTATION_STYLE_ASSIGNMENT((#100446));
#100484=STYLED_ITEM('',(#100447),#43720);
#100485=MECHANICAL_DESIGN_GEOMETRIC_PRESENTATION_REPRESENTATION('',(#100484),#45585);
ENDSEC;
END-ISO-10303-21;
